ISO-10303-21;
HEADER;
FILE_DESCRIPTION (('STEP AP214'),
    '1' );
FILE_NAME ('Snap Open Cable Crossbars 11.step',
    '2026-10-08T22:59:04',
    ( '' ),
    ( '' ),
    'SwSTEP 2.0',
    'SolidWorks 2020',
    '' );
FILE_SCHEMA (( 'AUTOMOTIVE_DESIGN' ));
ENDSEC;

DATA;
#29=DIRECTION ( 'NONE',  ( -1.020425574104004196E-15, -6.982962677686266711E-15, 1.000000000000000000 ) ) ;
#210=EDGE_CURVE ( 'NONE', #252512, #147282, #169419, .T. ) ;
#323=DIRECTION ( 'NONE',  ( -0.000000000000000000, -6.982962677686266711E-15, 1.000000000000000000 ) ) ;
#501=DIRECTION ( 'NONE',  ( 0.000000000000000000, -1.000000000000000000, -6.982962677686266711E-15 ) ) ;
#551=CARTESIAN_POINT ( 'NONE',  ( 18.39999999999999503, 64.25000000001253397, -179.2731074845244450 ) ) ;
#718=FACE_OUTER_BOUND ( 'NONE', #166984, .T. ) ;
#956=ORIENTED_EDGE ( 'NONE', *, *, #204565, .T. ) ;
#984=ADVANCED_FACE ( 'NONE', ( #247971 ), #13226, .T. ) ;
#1205=ORIENTED_EDGE ( 'NONE', *, *, #153700, .T. ) ;
#1263=AXIS2_PLACEMENT_3D ( 'NONE', #235738, #57082, #136631 ) ;
#1270=CARTESIAN_POINT ( 'NONE',  ( -17.01764560440403784, 66.05000000001263061, -190.7731074853133180 ) ) ;
#1568=CARTESIAN_POINT ( 'NONE',  ( -14.22969084473440304, 66.54399267394325079, -185.0344739903777054 ) ) ;
#1608=CARTESIAN_POINT ( 'NONE',  ( 14.45204356427542258, 66.54933111084504560, -188.4675609943170400 ) ) ;
#1742=CARTESIAN_POINT ( 'NONE',  ( -17.04761207306819060, 65.97354912661484150, -190.8731074845244109 ) ) ;
#1837=CARTESIAN_POINT ( 'NONE',  ( -17.01764560440408047, 66.05000000001255955, -182.7731074837355436 ) ) ;
#1854=PLANE ( 'NONE',  #71495 ) ;
#1933=DIRECTION ( 'NONE',  ( 0.000000000000000000, -6.982962677686266711E-15, 1.000000000000000000 ) ) ;
#2026=EDGE_CURVE ( 'NONE', #49183, #47477, #35737, .T. ) ;
#2344=ORIENTED_EDGE ( 'NONE', *, *, #168711, .T. ) ;
#2413=EDGE_LOOP ( 'NONE', ( #46517, #136076 ) ) ;
#2425=AXIS2_PLACEMENT_3D ( 'NONE', #153513, #135160, #16531 ) ;
#2493=VERTEX_POINT ( 'NONE', #41706 ) ;
#2846=CARTESIAN_POINT ( 'NONE',  ( 13.99999999999999822, 66.15000000001258229, -186.7731074845244450 ) ) ;
#2848=CARTESIAN_POINT ( 'NONE',  ( -12.60829076262180415, 66.61047060254583130, -185.7059995716306844 ) ) ;
#2878=VERTEX_POINT ( 'NONE', #41258 ) ;
#2991=DIRECTION ( 'NONE',  ( -0.7071067811865456854, -0.7071067811865493491, -4.937700262164544098E-15 ) ) ;
#3220=CARTESIAN_POINT ( 'NONE',  ( -16.87683809663752044, 66.05000000001255955, -183.4254715027207396 ) ) ;
#3391=VECTOR ( 'NONE', #82559, 1000.000000000000000 ) ;
#3569=ORIENTED_EDGE ( 'NONE', *, *, #71773, .F. ) ;
#3609=ORIENTED_EDGE ( 'NONE', *, *, #83186, .F. ) ;
#3696=VECTOR ( 'NONE', #121970, 1000.000000000000000 ) ;
#3910=CARTESIAN_POINT ( 'NONE',  ( -16.88460203013674388, 66.04524099677682614, -182.6572156749861904 ) ) ;
#4135=CARTESIAN_POINT ( 'NONE',  ( -21.65000000000000213, 66.05000000001261640, -190.7731074845244166 ) ) ;
#4454=VERTEX_POINT ( 'NONE', #157078 ) ;
#4460=DIRECTION ( 'NONE',  ( -1.000000000000000000, 0.000000000000000000, -0.000000000000000000 ) ) ;
#5245=VERTEX_POINT ( 'NONE', #204561 ) ;
#5401=CARTESIAN_POINT ( 'NONE',  ( -12.30589683808040746, 66.64325398293431135, -186.3197477631601942 ) ) ;
#5537=ORIENTED_EDGE ( 'NONE', *, *, #215031, .F. ) ;
#5544=DIRECTION ( 'NONE',  ( 1.000000000000000000, 0.000000000000000000, 0.000000000000000000 ) ) ;
#5610=DIRECTION ( 'NONE',  ( 0.000000000000000000, -1.000000000000000000, -6.982962677686266711E-15 ) ) ;
#5665=DIRECTION ( 'NONE',  ( -0.000000000000000000, -6.982962677686266711E-15, 1.000000000000000000 ) ) ;
#5787=CARTESIAN_POINT ( 'NONE',  ( 20.09999999999999787, 66.25000000001259082, -182.6731074845244223 ) ) ;
#6071=CARTESIAN_POINT ( 'NONE',  ( -21.65000000000000213, 68.75000000001261924, -190.8731074845244109 ) ) ;
#6125=ADVANCED_FACE ( 'NONE', ( #160234 ), #100197, .T. ) ;
#6146=DIRECTION ( 'NONE',  ( 1.000000000000000000, -1.186688945009009831E-16, -8.286604613020806758E-31 ) ) ;
#6227=ORIENTED_EDGE ( 'NONE', *, *, #161028, .F. ) ;
#6267=VERTEX_POINT ( 'NONE', #228216 ) ;
#6343=B_SPLINE_CURVE_WITH_KNOTS ( 'NONE', 3,
 ( #13492, #214255, #190869, #30495, #33091, #12220, #52594, #9620, #132143, #233820 ),
 .UNSPECIFIED., .F., .F.,
 ( 4, 3, 3, 4 ),
 ( 1.950915401637565782E-15, 8.145022132826850876E-06, 1.905645951092260044E-05, 2.061107371225642508E-05 ),
 .UNSPECIFIED. ) ;
#6633=DIRECTION ( 'NONE',  ( -0.000000000000000000, -6.982962677686266711E-15, 1.000000000000000000 ) ) ;
#6688=CARTESIAN_POINT ( 'NONE',  ( -18.40000000000000213, 70.35000000001255671, -182.6731074845243938 ) ) ;
#6836=ORIENTED_EDGE ( 'NONE', *, *, #72956, .F. ) ;
#6878=ORIENTED_EDGE ( 'NONE', *, *, #167330, .T. ) ;
#6974=CARTESIAN_POINT ( 'NONE',  ( 21.72449340488910607, 65.71604372252150483, -194.2731074845244166 ) ) ;
#7003=EDGE_CURVE ( 'NONE', #193731, #71999, #111015, .T. ) ;
#7012=FACE_OUTER_BOUND ( 'NONE', #241402, .T. ) ;
#7146=CARTESIAN_POINT ( 'NONE',  ( -16.94275863006528482, 66.01050395134502935, -182.6314101024478589 ) ) ;
#7348=DIRECTION ( 'NONE',  ( 1.186688945009010077E-16, 1.000000000000000000, 6.982962677686266711E-15 ) ) ;
#7434=EDGE_CURVE ( 'NONE', #147282, #2878, #15547, .T. ) ;
#7513=EDGE_CURVE ( 'NONE', #243580, #47477, #187861, .T. ) ;
#7529=ORIENTED_EDGE ( 'NONE', *, *, #241067, .F. ) ;
#7623=EDGE_CURVE ( 'NONE', #2878, #38279, #156455, .T. ) ;
#7717=ORIENTED_EDGE ( 'NONE', *, *, #161502, .T. ) ;
#7915=DIRECTION ( 'NONE',  ( -1.020425574104004196E-15, 6.982962677686266711E-15, -1.000000000000000000 ) ) ;
#7973=CARTESIAN_POINT ( 'NONE',  ( -16.89155683852258250, 66.05000000001261640, -190.2457356349850386 ) ) ;
#8146=DIRECTION ( 'NONE',  ( 1.000000000000000000, 0.000000000000000000, 0.000000000000000000 ) ) ;
#8299=PLANE ( 'NONE',  #36145 ) ;
#8305=VECTOR ( 'NONE', #207849, 1000.000000000000000 ) ;
#8393=CARTESIAN_POINT ( 'NONE',  ( -16.84981964351528916, 66.08268176591369070, -182.8927090985447705 ) ) ;
#8424=CARTESIAN_POINT ( 'NONE',  ( -16.86379686415369861, 66.02478224075944979, -190.9564973736146953 ) ) ;
#8454=CARTESIAN_POINT ( 'NONE',  ( -16.94052228080552425, 66.01372026691369399, -182.6327319818550450 ) ) ;
#8492=ORIENTED_EDGE ( 'NONE', *, *, #175157, .T. ) ;
#8777=DIRECTION ( 'NONE',  ( 1.186688945009010077E-16, 1.000000000000000000, 6.982962677686266711E-15 ) ) ;
#9225=LINE ( 'NONE', #90039, #247305 ) ;
#9239=CARTESIAN_POINT ( 'NONE',  ( -16.88783316861810491, 66.05000000001261640, -190.7708434425451003 ) ) ;
#9365=ORIENTED_EDGE ( 'NONE', *, *, #229920, .F. ) ;
#9493=CARTESIAN_POINT ( 'NONE',  ( -16.77683809663752257, 52.34166666667924517, -186.7731074845245303 ) ) ;
#9601=AXIS2_PLACEMENT_3D ( 'NONE', #52207, #110911, #48366 ) ;
#9620=CARTESIAN_POINT ( 'NONE',  ( -16.87435696428308063, 66.04999753708037247, -190.8731157193578554 ) ) ;
#9885=CARTESIAN_POINT ( 'NONE',  ( -15.75000000000000355, 66.65000000001258229, -186.7731074845243882 ) ) ;
#10151=CARTESIAN_POINT ( 'NONE',  ( -16.78493832629888161, 66.05416425680844839, -190.8591584654202506 ) ) ;
#10171=AXIS2_PLACEMENT_3D ( 'NONE', #183124, #4460, #166155 ) ;
#10195=EDGE_CURVE ( 'NONE', #252537, #5245, #88131, .T. ) ;
#10432=CARTESIAN_POINT ( 'NONE',  ( -18.40000000000000213, 67.17743825834622839, -194.2731074845244166 ) ) ;
#10463=ADVANCED_FACE ( 'NONE', ( #252939 ), #16922, .F. ) ;
#10899=EDGE_CURVE ( 'NONE', #216617, #26389, #255055, .T. ) ;
#11003=ORIENTED_EDGE ( 'NONE', *, *, #205832, .F. ) ;
#11016=CARTESIAN_POINT ( 'NONE',  ( -17.11825945287482753, 66.05000000001261640, -190.7731074845244166 ) ) ;
#11076=EDGE_CURVE ( 'NONE', #180338, #85330, #171545, .T. ) ;
#11125=FILL_AREA_STYLE ('',( #89351 ) ) ;
#11161=EDGE_CURVE ( 'NONE', #213303, #199626, #93250, .T. ) ;
#11274=CARTESIAN_POINT ( 'NONE',  ( -16.80939487329394666, 66.05000000001255955, -182.6731074845235412 ) ) ;
#11352=( BOUNDED_CURVE ( )  B_SPLINE_CURVE ( 3, ( #200043, #138732, #44816, #124360 ),
 .UNSPECIFIED., .F., .F. ) 
 B_SPLINE_CURVE_WITH_KNOTS ( ( 4, 4 ),
 ( 5.733388419619902088, 5.983100554402347449 ),
 .UNSPECIFIED. ) 
 CURVE ( )  GEOMETRIC_REPRESENTATION_ITEM ( )  RATIONAL_B_SPLINE_CURVE ( ( 1.000000000000000000, 0.9948104011409417691, 0.9948104011409417691, 1.000000000000000000 ) ) 
 REPRESENTATION_ITEM ( '' )  );
#11425=EDGE_CURVE ( 'NONE', #256760, #54689, #17967, .T. ) ;
#11432=ADVANCED_FACE ( 'NONE', ( #28861 ), #121396, .F. ) ;
#11755=ORIENTED_EDGE ( 'NONE', *, *, #7623, .F. ) ;
#11926=ORIENTED_EDGE ( 'NONE', *, *, #161545, .T. ) ;
#12220=CARTESIAN_POINT ( 'NONE',  ( -16.87851181299898684, 66.04995707600485844, -190.8732509998913258 ) ) ;
#12253=DIRECTION ( 'NONE',  ( -0.000000000000000000, -6.982962677686266711E-15, 1.000000000000000000 ) ) ;
#12280=ORIENTED_EDGE ( 'NONE', *, *, #103050, .F. ) ;
#12283=VECTOR ( 'NONE', #82632, 1000.000000000000000 ) ;
#12427=( NAMED_UNIT ( * ) PLANE_ANGLE_UNIT ( ) SI_UNIT ( $, .RADIAN. ) );
#12548=VECTOR ( 'NONE', #184267, 999.9999999999998863 ) ;
#12556=ORIENTED_EDGE ( 'NONE', *, *, #172456, .F. ) ;
#12562=CARTESIAN_POINT ( 'NONE',  ( -16.77732147278574715, 66.05403306743916403, -190.8595987276486312 ) ) ;
#12601=ADVANCED_FACE ( 'NONE', ( #143969 ), #108713, .F. ) ;
#12926=CARTESIAN_POINT ( 'NONE',  ( -16.92507428761699018, 66.05000000001255955, -182.7365049441459917 ) ) ;
#13061=CARTESIAN_POINT ( 'NONE',  ( -16.81453563122428108, 66.06089979457560446, -182.7348488238791901 ) ) ;
#13226=( BOUNDED_SURFACE ( )  B_SPLINE_SURFACE ( 3, 2, ( 
 ( #69361, #133174, #90168 ),
 ( #129318, #109736, #193158 ),
 ( #14534, #151473, #211424 ),
 ( #189301, #169770, #150181 ) ),
 .UNSPECIFIED., .F., .F., .T. ) 
 B_SPLINE_SURFACE_WITH_KNOTS ( ( 4, 4 ),
 ( 3, 3 ),
 ( 0.0008258556059633759532, 0.0009616864997632701634 ),
 ( 0.000000000000000000, 1.000000000000000000 ),
 .UNSPECIFIED. ) 
 GEOMETRIC_REPRESENTATION_ITEM ( )  RATIONAL_B_SPLINE_SURFACE ( (
 ( 1.000000000000000000, 0.9152888060719485130, 1.000000000000000000),
 ( 1.000000000000000000, 0.9327727094138390518, 1.000000000000000000),
 ( 1.000000000000000000, 0.9369023509257937699, 1.000000000000000000),
 ( 1.000000000000000000, 0.9246339933864583527, 1.000000000000000000) ) ) 
 REPRESENTATION_ITEM ( '' )  SURFACE ( )  );
#13472=VERTEX_POINT ( 'NONE', #254917 ) ;
#13492=CARTESIAN_POINT ( 'NONE',  ( -16.89268316805466341, 66.04827818677041762, -190.8788599630699707 ) ) ;
#13638=ORIENTED_EDGE ( 'NONE', *, *, #226393, .F. ) ;
#13699=ORIENTED_EDGE ( 'NONE', *, *, #208678, .T. ) ;
#13841=CARTESIAN_POINT ( 'NONE',  ( -16.80117486205003630, 66.05034273170022630, -182.6742526115989449 ) ) ;
#14534=CARTESIAN_POINT ( 'NONE',  ( -16.92973740335405708, 66.00749618554552001, -190.9291665197260386 ) ) ;
#14975=DIRECTION ( 'NONE',  ( -0.5932847527679298016, -0.8049926720990051576, -5.621233785078291429E-15 ) ) ;
#15025=EDGE_LOOP ( 'NONE', ( #231027, #216368, #167552, #55140 ) ) ;
#15338=CARTESIAN_POINT ( 'NONE',  ( 18.54999999999999716, 67.25000000001257661, -190.8731074845244109 ) ) ;
#15465=ORIENTED_EDGE ( 'NONE', *, *, #206902, .F. ) ;
#15547=CIRCLE ( 'NONE', #111202, 0.5000000000000004441 ) ;
#15637=CARTESIAN_POINT ( 'NONE',  ( -16.83199318825828072, 66.06935387203138532, -182.7955222963152266 ) ) ;
#15789=ORIENTED_EDGE ( 'NONE', *, *, #172367, .F. ) ;
#15887=ORIENTED_EDGE ( 'NONE', *, *, #163950, .T. ) ;
#16172=LINE ( 'NONE', #137358, #236369 ) ;
#16527=CARTESIAN_POINT ( 'NONE',  ( -18.38817693311004575, 64.51850848411275763, -179.2731074845244450 ) ) ;
#16531=DIRECTION ( 'NONE',  ( 1.000000000000000000, 0.000000000000000000, 0.000000000000000000 ) ) ;
#16680=LINE ( 'NONE', #238265, #137182 ) ;
#16806=DIRECTION ( 'NONE',  ( -3.035766082959430717E-14, -6.982962677686266711E-15, 1.000000000000000000 ) ) ;
#16835=CARTESIAN_POINT ( 'NONE',  ( -16.93262454970419384, 65.99797953208218360, -182.5960312582870984 ) ) ;
#16898=CARTESIAN_POINT ( 'NONE',  ( -33.72168855820452649, 52.34166666667924517, -186.7731074845245303 ) ) ;
#16922=PLANE ( 'NONE',  #213235 ) ;
#16967=CARTESIAN_POINT ( 'NONE',  ( -16.77180007708461673, 66.05000000001261640, -190.8874933655695827 ) ) ;
#17076=ORIENTED_EDGE ( 'NONE', *, *, #34634, .F. ) ;
#17235=EDGE_CURVE ( 'NONE', #23645, #221894, #142556, .T. ) ;
#17472=CARTESIAN_POINT ( 'NONE',  ( -23.25000000000000355, 70.35000000001255671, -182.6731074845243938 ) ) ;
#17680=ADVANCED_FACE ( 'NONE', ( #206099 ), #125283, .F. ) ;
#17726=DIRECTION ( 'NONE',  ( 1.000000000000000000, 0.000000000000000000, 0.000000000000000000 ) ) ;
#17967=CIRCLE ( 'NONE', #9601, 0.1000000000000028644 ) ;
#18061=CARTESIAN_POINT ( 'NONE',  ( -21.64999999999999858, 65.95000000001260787, -190.7731074845244166 ) ) ;
#18319=VERTEX_POINT ( 'NONE', #79085 ) ;
#18444=ORIENTED_EDGE ( 'NONE', *, *, #148203, .F. ) ;
#18640=B_SPLINE_CURVE_WITH_KNOTS ( 'NONE', 3,
 ( #149627, #257619, #38645, #154762, #16527, #119473, #234259 ),
 .UNSPECIFIED., .F., .F.,
 ( 4, 3, 4 ),
 ( 3.469446951953614189E-18, 3.882884552234413736E-05, 5.798605692158458936E-05 ),
 .UNSPECIFIED. ) ;
#18775=CARTESIAN_POINT ( 'NONE',  ( 18.54999999999999716, 67.25000000001251976, -182.6731074845244223 ) ) ;
#18812=B_SPLINE_CURVE_WITH_KNOTS ( 'NONE', 3,
 ( #238959, #198531, #60296, #21216, #98114, #235104, #19916, #78579, #137268, #194713, #79844, #158174, #138531, #39501, #255888, #1608, #135974, #156875, #141141, #40781, #119013, #236375, #159426, #100682, #199844, #220672 ),
 .UNSPECIFIED., .F., .F.,
 ( 4, 2, 2, 2, 2, 2, 2, 2, 2, 2, 2, 2, 4 ),
 ( 0.005476422646581303143, 0.006160811967703551384, 0.006845201288825798758, 0.007187395949386892954, 0.007529590609947988886, 0.007871785270509083082, 0.008213979931070177279, 0.008556174591631273210, 0.008898369252192367407, 0.009240563912753461603, 0.009582758573314555800, 0.01026714789443679970, 0.01095153721555904534 ),
 .UNSPECIFIED. ) ;
#18948=CARTESIAN_POINT ( 'NONE',  ( -16.87036670365548474, 66.01058118071088643, -182.5435473672224020 ) ) ;
#19046=EDGE_CURVE ( 'NONE', #26389, #92187, #207127, .T. ) ;
#19202=CARTESIAN_POINT ( 'NONE',  ( -17.01473183483381391, 66.05000000001261640, -190.7731074845244166 ) ) ;
#19571=ADVANCED_FACE ( 'NONE', ( #30759 ), #155363, .T. ) ;
#19626=DIRECTION ( 'NONE',  ( 1.000000000000000000, 0.000000000000000000, 0.000000000000000000 ) ) ;
#19787=VECTOR ( 'NONE', #93831, 1000.000000000000000 ) ;
#19882=CARTESIAN_POINT ( 'NONE',  ( -15.74999999999999645, 66.65000000001256808, -186.6588398769082460 ) ) ;
#19916=CARTESIAN_POINT ( 'NONE',  ( 12.93225390519043394, 66.58234804117158490, -188.1643200920839547 ) ) ;
#20028=DIRECTION ( 'NONE',  ( 1.000000000000000000, 7.492892343619937423E-30, -1.073024830501117725E-15 ) ) ;
#20096=CARTESIAN_POINT ( 'NONE',  ( -16.91247567987038281, 66.04091731634333939, -190.8943830259870822 ) ) ;
#20205=CARTESIAN_POINT ( 'NONE',  ( -16.87036670365549895, 66.01058118071095748, -191.0026676018264880 ) ) ;
#20338=CARTESIAN_POINT ( 'NONE',  ( -18.37013991200266361, 64.50025238380054304, -179.2300844740073273 ) ) ;
#20416=CARTESIAN_POINT ( 'NONE',  ( 20.09999999999999787, 66.25000000001264766, -194.2731074845244166 ) ) ;
#20809=VECTOR ( 'NONE', #218604, 1000.000000000000000 ) ;
#20989=CARTESIAN_POINT ( 'NONE',  ( 15.57250062127603663, 66.62931007840995790, -185.9966423578633794 ) ) ;
#21182=CARTESIAN_POINT ( 'NONE',  ( -15.31895204843004699, 66.60346600605865319, -185.6171677053510791 ) ) ;
#21216=CARTESIAN_POINT ( 'NONE',  ( 12.47034474403011473, 66.62446189796457929, -187.6532316035335839 ) ) ;
#21405=ORIENTED_EDGE ( 'NONE', *, *, #152556, .F. ) ;
#21521=PLANE ( 'NONE',  #196153 ) ;
#21613=CARTESIAN_POINT ( 'NONE',  ( -16.87036670365547408, 66.01058118071090064, -182.5435473672224305 ) ) ;
#21636=CARTESIAN_POINT ( 'NONE',  ( -18.40000000000000213, 64.52683809665013825, -190.9145288407617613 ) ) ;
#22033=DIRECTION ( 'NONE',  ( 0.000000000000000000, 0.000000000000000000, 1.000000000000000000 ) ) ;
#22051=LINE ( 'NONE', #242358, #250706 ) ;
#22509=EDGE_LOOP ( 'NONE', ( #123737, #24257, #176427, #24129, #167078, #198883, #70180, #212052, #185227, #104237 ) ) ;
#22522=FACE_OUTER_BOUND ( 'NONE', #203132, .T. ) ;
#22564=EDGE_LOOP ( 'NONE', ( #193218, #224737, #75319, #132310, #36146 ) ) ;
#22843=CARTESIAN_POINT ( 'NONE',  ( -16.87683809663752399, 66.15000000001259650, -190.1207434663281219 ) ) ;
#22888=CARTESIAN_POINT ( 'NONE',  ( -16.97048326478264357, 66.05000000001264482, -190.3820006043973194 ) ) ;
#22912=CARTESIAN_POINT ( 'NONE',  ( -17.80356949364066566, 65.12326860300937881, -180.3100344602943039 ) ) ;
#22937=EDGE_CURVE ( 'NONE', #239104, #147282, #16680, .T. ) ;
#23076=ORIENTED_EDGE ( 'NONE', *, *, #77298, .T. ) ;
#23095=CARTESIAN_POINT ( 'NONE',  ( -18.40000000000000213, 64.52683809665005299, -182.5731074845244279 ) ) ;
#23328=ORIENTED_EDGE ( 'NONE', *, *, #114492, .F. ) ;
#23455=CARTESIAN_POINT ( 'NONE',  ( -16.91049119928363353, 66.05000000001263061, -190.9048278777152632 ) ) ;
#23476=ORIENTED_EDGE ( 'NONE', *, *, #219166, .F. ) ;
#23645=VERTEX_POINT ( 'NONE', #56115 ) ;
#23662=CARTESIAN_POINT ( 'NONE',  ( 20.73486653747088937, 68.25000000001251976, -182.6731074845244223 ) ) ;
#23750=CARTESIAN_POINT ( 'NONE',  ( -12.48127053791144725, 66.62341902196861554, -185.8961612375124446 ) ) ;
#23961=ADVANCED_FACE ( 'NONE', ( #22522 ), #137607, .T. ) ;
#24100=DIRECTION ( 'NONE',  ( 0.000000000000000000, 1.000000000000000000, 6.982962677686266711E-15 ) ) ;
#24115=CARTESIAN_POINT ( 'NONE',  ( -16.77431908686106965, 66.05419424549457119, -182.6872682668742129 ) ) ;
#24129=ORIENTED_EDGE ( 'NONE', *, *, #208678, .F. ) ;
#24173=CARTESIAN_POINT ( 'NONE',  ( -16.94389599337535657, 66.00880201025582039, -182.6307522863228314 ) ) ;
#24257=ORIENTED_EDGE ( 'NONE', *, *, #245413, .T. ) ;
#24375=VERTEX_POINT ( 'NONE', #45616 ) ;
#25450=CARTESIAN_POINT ( 'NONE',  ( -14.77738660682464911, 66.56344716000816675, -188.3451520117640996 ) ) ;
#25590=ORIENTED_EDGE ( 'NONE', *, *, #7003, .T. ) ;
#25612=DIRECTION ( 'NONE',  ( 0.000000000000000000, -1.000000000000000000, -6.982962677686266711E-15 ) ) ;
#25638=LINE ( 'NONE', #63464, #206659 ) ;
#25995=ORIENTED_EDGE ( 'NONE', *, *, #214896, .F. ) ;
#26123=CARTESIAN_POINT ( 'NONE',  ( -16.93433913041102912, 65.99402157848859929, -182.5877420571292760 ) ) ;
#26290=DIRECTION ( 'NONE',  ( 1.000000000000000000, 0.000000000000000000, 0.000000000000000000 ) ) ;
#26389=VERTEX_POINT ( 'NONE', #64743 ) ;
#26449=CARTESIAN_POINT ( 'NONE',  ( -16.94445028196807002, 66.00793639031481064, -182.6304376629428816 ) ) ;
#26507=AXIS2_PLACEMENT_3D ( 'NONE', #213152, #114044, #14975 ) ;
#26750=CARTESIAN_POINT ( 'NONE',  ( -16.93935632781549572, 66.01526950028744523, -182.6334467358141467 ) ) ;
#26931=ORIENTED_EDGE ( 'NONE', *, *, #70916, .F. ) ;
#26999=CARTESIAN_POINT ( 'NONE',  ( -18.40000000000000213, 64.25000000001256240, -182.6731074845244507 ) ) ;
#27320=CARTESIAN_POINT ( 'NONE',  ( 15.74999999999999645, 66.65000000001258229, -186.7731074845244166 ) ) ;
#27351=CARTESIAN_POINT ( 'NONE',  ( 18.39999999999997371, 64.52683809665003878, -179.2731074845244450 ) ) ;
#27437=CARTESIAN_POINT ( 'NONE',  ( -16.93826681692523195, 65.98857127972483738, -182.5776490171649868 ) ) ;
#27472=EDGE_LOOP ( 'NONE', ( #146370, #115933, #79267, #220770 ) ) ;
#27584=PLANE ( 'NONE',  #81770 ) ;
#27592=DIRECTION ( 'NONE',  ( -0.000000000000000000, -6.982962677686266711E-15, 1.000000000000000000 ) ) ;
#27742=ORIENTED_EDGE ( 'NONE', *, *, #256767, .T. ) ;
#27762=ORIENTED_EDGE ( 'NONE', *, *, #7434, .F. ) ;
#27980=CARTESIAN_POINT ( 'NONE',  ( -16.87683809663752399, 66.13411015068015786, -183.2905342915938149 ) ) ;
#28039=LINE ( 'NONE', #204063, #92126 ) ;
#28527=CARTESIAN_POINT ( 'NONE',  ( 20.27550659511088682, 66.78395627750374786, -190.8731074845244393 ) ) ;
#28811=DIRECTION ( 'NONE',  ( 0.7071067811865463515, 0.7071067811865487940, 4.937700262164540154E-15 ) ) ;
#28818=DIRECTION ( 'NONE',  ( -0.000000000000000000, -6.982962677686266711E-15, 1.000000000000000000 ) ) ;
#28861=FACE_OUTER_BOUND ( 'NONE', #210231, .T. ) ;
#29248=EDGE_CURVE ( 'NONE', #74091, #67839, #194476, .T. ) ;
#29260=EDGE_CURVE ( 'NONE', #54771, #75787, #202438, .T. ) ;
#29333=ORIENTED_EDGE ( 'NONE', *, *, #174875, .T. ) ;
#29549=AXIS2_PLACEMENT_3D ( 'NONE', #142030, #44234, #221545 ) ;
#29678=AXIS2_PLACEMENT_3D ( 'NONE', #209273, #34518, #154481 ) ;
#29744=CARTESIAN_POINT ( 'NONE',  ( -16.77683809663752257, 66.05416425680844839, -190.8591584654202222 ) ) ;
#29997=ORIENTED_EDGE ( 'NONE', *, *, #167330, .F. ) ;
#30005=ORIENTED_EDGE ( 'NONE', *, *, #206902, .T. ) ;
#30006=ORIENTED_EDGE ( 'NONE', *, *, #254181, .T. ) ;
#30071=B_SPLINE_CURVE_WITH_KNOTS ( 'NONE', 3,
 ( #41060, #198816, #218360, #39782 ),
 .UNSPECIFIED., .F., .F.,
 ( 4, 4 ),
 ( 0.000000000000000000, 7.713889350930119414E-05 ),
 .UNSPECIFIED. ) ;
#30115=CARTESIAN_POINT ( 'NONE',  ( -16.85722902420150504, 66.05000000001261640, -190.7575600107546165 ) ) ;
#30153=LINE ( 'NONE', #71848, #191363 ) ;
#30227=ORIENTED_EDGE ( 'NONE', *, *, #69954, .T. ) ;
#30276=DIRECTION ( 'NONE',  ( 1.000000000000000000, 0.000000000000000000, 0.000000000000000000 ) ) ;
#30432=CARTESIAN_POINT ( 'NONE',  ( -17.11825945287481687, 65.95000000001255103, -182.6731074845244507 ) ) ;
#30495=CARTESIAN_POINT ( 'NONE',  ( -16.88560720703333473, 66.04943515626290207, -190.8749955636607183 ) ) ;
#30620=ORIENTED_EDGE ( 'NONE', *, *, #137104, .F. ) ;
#30759=FACE_OUTER_BOUND ( 'NONE', #205271, .T. ) ;
#30998=CARTESIAN_POINT ( 'NONE',  ( 23.24999999999999645, 64.25000000001261924, -190.8731074845244393 ) ) ;
#31167=( BOUNDED_SURFACE ( )  B_SPLINE_SURFACE ( 3, 2, ( 
 ( #97788, #177393, #241202 ),
 ( #1270, #80800, #122536 ),
 ( #256836, #102934, #160393 ),
 ( #202064, #23455, #255557 ) ),
 .UNSPECIFIED., .F., .F., .F. ) 
 B_SPLINE_SURFACE_WITH_KNOTS ( ( 4, 4 ),
 ( 3, 3 ),
 ( 4.712388980384689674, 5.765869716888531116 ),
 ( 0.000000000000000000, 1.000000000000000000 ),
 .UNSPECIFIED. ) 
 GEOMETRIC_REPRESENTATION_ITEM ( )  RATIONAL_B_SPLINE_SURFACE ( (
 ( 1.000000000000000000, 0.7071067811866457165, 1.000000000000000000),
 ( 1.000000000000000000, 0.7953136715912294541, 1.000000000000000000),
 ( 1.000000000000000000, 0.8646876308616092688, 1.000000000000000000),
 ( 1.000000000000000000, 0.8984936768950676500, 1.000000000000000000) ) ) 
 REPRESENTATION_ITEM ( '' )  SURFACE ( )  );
#31526=ORIENTED_EDGE ( 'NONE', *, *, #238961, .T. ) ;
#31747=DIRECTION ( 'NONE',  ( -1.073024830501117725E-15, 6.982962677686266711E-15, -1.000000000000000000 ) ) ;
#31988=PRESENTATION_STYLE_ASSIGNMENT (( #145486 ) ) ;
#32017=CARTESIAN_POINT ( 'NONE',  ( -23.25000000000000355, 70.35000000001261355, -190.8731074845244109 ) ) ;
#32174=VECTOR ( 'NONE', #192680, 1000.000000000000000 ) ;
#32262=EDGE_LOOP ( 'NONE', ( #187378, #115472, #187313, #6227, #192933 ) ) ;
#32334=VECTOR ( 'NONE', #323, 1000.000000000000000 ) ;
#32444=ORIENTED_EDGE ( 'NONE', *, *, #238961, .F. ) ;
#32569=CARTESIAN_POINT ( 'NONE',  ( -16.93860193097148326, 66.00689223268328476, -182.6229691172175933 ) ) ;
#33091=CARTESIAN_POINT ( 'NONE',  ( -16.88219499860498374, 66.04979357458500999, -190.8737977944171291 ) ) ;
#33188=CARTESIAN_POINT ( 'NONE',  ( -12.47155713865592119, 66.62433047358680938, -187.6553174751384745 ) ) ;
#33331=DIRECTION ( 'NONE',  ( -0.000000000000000000, -6.982962677686266711E-15, 1.000000000000000000 ) ) ;
#33338=CARTESIAN_POINT ( 'NONE',  ( -17.80356949363508079, 65.12326860301504894, -193.2361805087437006 ) ) ;
#33388=ORIENTED_EDGE ( 'NONE', *, *, #230937, .F. ) ;
#33652=EDGE_LOOP ( 'NONE', ( #243868, #134091, #247997, #21405 ) ) ;
#33851=ORIENTED_EDGE ( 'NONE', *, *, #161028, .T. ) ;
#33937=CARTESIAN_POINT ( 'NONE',  ( -16.78493211734303614, 66.05416425680837733, -182.6870565036285257 ) ) ;
#33960=DIRECTION ( 'NONE',  ( 0.000000000000000000, 1.000000000000000000, 6.982962677686266711E-15 ) ) ;
#34229=DIRECTION ( 'NONE',  ( 1.000000000000000000, 0.000000000000000000, 0.000000000000000000 ) ) ;
#34256=( BOUNDED_CURVE ( )  B_SPLINE_CURVE ( 3, ( #79982, #1742, #120461, #160855 ),
 .UNSPECIFIED., .F., .F. ) 
 B_SPLINE_CURVE_WITH_KNOTS ( ( 4, 4 ),
 ( 4.712388980384690562, 5.672655318024762749 ),
 .UNSPECIFIED. ) 
 CURVE ( )  GEOMETRIC_REPRESENTATION_ITEM ( )  RATIONAL_B_SPLINE_CURVE ( ( 1.000000000000000000, 0.9246222802177245237, 0.9246222802177245237, 1.000000000000000000 ) ) 
 REPRESENTATION_ITEM ( '' )  );
#34337=AXIS2_PLACEMENT_3D ( 'NONE', #16898, #174728, #254191 ) ;
#34436=EDGE_CURVE ( 'NONE', #2493, #178117, #99331, .T. ) ;
#34507=VECTOR ( 'NONE', #243308, 1000.000000000000000 ) ;
#34518=DIRECTION ( 'NONE',  ( -1.000000000000000000, -7.125593699324843413E-30, 1.020425574104004196E-15 ) ) ;
#34544=FACE_OUTER_BOUND ( 'NONE', #15025, .T. ) ;
#34634=EDGE_CURVE ( 'NONE', #110389, #178700, #183425, .T. ) ;
#34707=CARTESIAN_POINT ( 'NONE',  ( -16.78270389226384651, 66.05262738339554573, -182.6819004476129464 ) ) ;
#34873=CARTESIAN_POINT ( 'NONE',  ( -16.83794237512072911, 66.07364077890511567, -190.7195653258254708 ) ) ;
#34996=( BOUNDED_SURFACE ( )  B_SPLINE_SURFACE ( 3, 2, ( 
 ( #48783, #3220, #206579 ),
 ( #27980, #187044, #204005 ),
 ( #103598, #107476, #65782 ),
 ( #166207, #145304, #224846 ),
 ( #8393, #82737, #87885 ),
 ( #162336, #167479, #246980 ),
 ( #241845, #46210, #63193 ),
 ( #147903, #67072, #227419 ),
 ( #142733, #123193, #202718 ),
 ( #24115, #163607, #243131 ) ),
 .UNSPECIFIED., .F., .F., .F. ) 
 B_SPLINE_SURFACE_WITH_KNOTS ( ( 4, 2, 2, 2, 4 ),
 ( 3, 3 ),
 ( 0.002161241639767276426, 0.002579950749615843482, 0.002789305304540127227, 0.002893982582002269099, 0.002998659859464410972 ),
 ( 0.000000000000000000, 1.000000000000000000 ),
 .UNSPECIFIED. ) 
 GEOMETRIC_REPRESENTATION_ITEM ( )  RATIONAL_B_SPLINE_SURFACE ( (
 ( 1.000000000000000000, 0.7071067811865475727, 1.000000000000000000),
 ( 1.000000000000000000, 0.7632447400664224002, 1.000000000000000000),
 ( 1.000000000000000000, 0.8158073005110438869, 1.000000000000000000),
 ( 1.000000000000000000, 0.8906973462395797458, 1.000000000000000000),
 ( 1.000000000000000000, 0.9149408947802050163, 1.000000000000000000),
 ( 1.000000000000000000, 0.9493368785274935995, 1.000000000000000000),
 ( 1.000000000000000000, 0.9605194247157773368, 1.000000000000000000),
 ( 1.000000000000000000, 0.9803630264780145431, 1.000000000000000000),
 ( 1.000000000000000000, 0.9900844824271928246, 1.000000000000000000),
 ( 1.000000000000000000, 0.9894588281429246290, 1.000000000000000000) ) ) 
 REPRESENTATION_ITEM ( '' )  SURFACE ( )  );
#35022=PLANE ( 'NONE',  #199907 ) ;
#35171=CARTESIAN_POINT ( 'NONE',  ( -16.87331047859651179, 66.05000000001261640, -190.8731074845244393 ) ) ;
#35268=CARTESIAN_POINT ( 'NONE',  ( -16.77431908686106965, 66.05419424549462803, -190.8589467021746486 ) ) ;
#35495=AXIS2_PLACEMENT_3D ( 'NONE', #72900, #190260, #191561 ) ;
#35737=LINE ( 'NONE', #112682, #205398 ) ;
#35762=ORIENTED_EDGE ( 'NONE', *, *, #212001, .F. ) ;
#35887=CARTESIAN_POINT ( 'NONE',  ( -17.27223548802716380, 65.65460260865593511, -192.1567136637387705 ) ) ;
#35903=CARTESIAN_POINT ( 'NONE',  ( -20.65000000000000568, 68.75000000001261924, -190.8731074845244109 ) ) ;
#35928=ORIENTED_EDGE ( 'NONE', *, *, #88736, .F. ) ;
#35981=ORIENTED_EDGE ( 'NONE', *, *, #83186, .T. ) ;
#36145=AXIS2_PLACEMENT_3D ( 'NONE', #188207, #126949, #168695 ) ;
#36146=ORIENTED_EDGE ( 'NONE', *, *, #129599, .F. ) ;
#36423=EDGE_LOOP ( 'NONE', ( #87802, #122295, #91640, #112261, #25590, #232539, #30227, #172643, #1205, #186695, #234743, #12280, #256000, #88334, #173716, #90715, #143444, #178359 ) ) ;
#36511=EDGE_CURVE ( 'NONE', #242970, #199921, #115035, .T. ) ;
#36544=VERTEX_POINT ( 'NONE', #56324 ) ;
#36602=DIRECTION ( 'NONE',  ( 0.000000000000000000, -6.982962677686266711E-15, 1.000000000000000000 ) ) ;
#36874=LINE ( 'NONE', #177664, #240976 ) ;
#36968=EDGE_CURVE ( 'NONE', #232210, #63287, #208115, .T. ) ;
#37146=CARTESIAN_POINT ( 'NONE',  ( -15.55912972643740488, 67.50912972644997012, -182.6731074845244223 ) ) ;
#37527=AXIS2_PLACEMENT_3D ( 'NONE', #237654, #218060, #99398 ) ;
#37755=FACE_BOUND ( 'NONE', #165345, .T. ) ;
#37780=DIRECTION ( 'NONE',  ( 0.000000000000000000, 6.982962677686266711E-15, -1.000000000000000000 ) ) ;
#37927=ORIENTED_EDGE ( 'NONE', *, *, #227766, .T. ) ;
#38050=CARTESIAN_POINT ( 'NONE',  ( -18.40000000000000213, 64.52683809665012404, -190.9731074845244621 ) ) ;
#38257=CARTESIAN_POINT ( 'NONE',  ( -16.93262454970420094, 65.99797953208224044, -190.9501837107617632 ) ) ;
#38279=VERTEX_POINT ( 'NONE', #58164 ) ;
#38521=CARTESIAN_POINT ( 'NONE',  ( -23.25000000000000355, 64.25000000001264766, -194.2731074845244450 ) ) ;
#38642=ORIENTED_EDGE ( 'NONE', *, *, #206763, .F. ) ;
#38645=CARTESIAN_POINT ( 'NONE',  ( -18.36973785203555920, 64.52449679952829342, -179.2731074845244450 ) ) ;
#38654=ORIENTED_EDGE ( 'NONE', *, *, #57799, .F. ) ;
#38684=ORIENTED_EDGE ( 'NONE', *, *, #22937, .F. ) ;
#38876=ORIENTED_EDGE ( 'NONE', *, *, #77298, .F. ) ;
#38902=DIRECTION ( 'NONE',  ( -1.000000000000000000, -0.000000000000000000, -0.000000000000000000 ) ) ;
#39232=FACE_OUTER_BOUND ( 'NONE', #2413, .T. ) ;
#39278=CARTESIAN_POINT ( 'NONE',  ( 20.09999999999999787, 66.25000000001259082, -190.8731074845244393 ) ) ;
#39405=DIRECTION ( 'NONE',  ( 0.000000000000000000, -1.000000000000000000, -6.982962677686266711E-15 ) ) ;
#39466=CARTESIAN_POINT ( 'NONE',  ( -15.39126916658603861, 66.61042836546617707, -185.7054667721552903 ) ) ;
#39501=CARTESIAN_POINT ( 'NONE',  ( 14.11444803880197441, 66.54256847116367624, -188.5231905466248179 ) ) ;
#39569=CARTESIAN_POINT ( 'NONE',  ( -16.93583594267724379, 65.99137656496040449, -190.9637166452036752 ) ) ;
#39782=CARTESIAN_POINT ( 'NONE',  ( -18.40000000000000213, 64.52683809665003878, -179.3490535513324176 ) ) ;
#40011=AXIS2_PLACEMENT_3D ( 'NONE', #53482, #168339, #233422 ) ;
#40748=CARTESIAN_POINT ( 'NONE',  ( -12.25000000000000178, 66.15000000001258229, -186.7731074845244166 ) ) ;
#40750=CARTESIAN_POINT ( 'NONE',  ( -12.92414019175887141, 66.58236703690630520, -185.3741590187921986 ) ) ;
#40781=CARTESIAN_POINT ( 'NONE',  ( 15.06592377766032342, 66.58221053306037618, -188.1657229405476812 ) ) ;
#40847=CARTESIAN_POINT ( 'NONE',  ( -16.93970660449832621, 65.98715860837702962, -190.9708257487299363 ) ) ;
#40948=CARTESIAN_POINT ( 'NONE',  ( -18.40000000000000213, 70.35000000001255671, -182.6731074845243938 ) ) ;
#41060=CARTESIAN_POINT ( 'NONE',  ( -18.40000000000000213, 64.51332499825484490, -179.2731074845244450 ) ) ;
#41141=VECTOR ( 'NONE', #33960, 1000.000000000000000 ) ;
#41178=CARTESIAN_POINT ( 'NONE',  ( -14.11697426661282684, 66.54258905524518752, -188.5230235107343901 ) ) ;
#41258=CARTESIAN_POINT ( 'NONE',  ( 21.13736287352038445, 67.95335762362854837, -182.6731074845244223 ) ) ;
#41376=ORIENTED_EDGE ( 'NONE', *, *, #168711, .F. ) ;
#41706=CARTESIAN_POINT ( 'NONE',  ( -16.97683809663752186, 66.05000000001261640, -190.1207434663279514 ) ) ;
#41944=DIRECTION ( 'NONE',  ( -1.646408749285562691E-14, -1.000000000000000000, -6.982962677686266711E-15 ) ) ;
#42047=ORIENTED_EDGE ( 'NONE', *, *, #167538, .T. ) ;
#42098=SURFACE_SIDE_STYLE ('',( #61638 ) ) ;
#42226=CARTESIAN_POINT ( 'NONE',  ( -16.89268316805466341, 66.04827818677041762, -190.8788599630699707 ) ) ;
#42284=CARTESIAN_POINT ( 'NONE',  ( -17.11825945287481687, 66.05000000001255955, -182.6731074845244507 ) ) ;
#42417=ORIENTED_EDGE ( 'NONE', *, *, #236978, .F. ) ;
#42425=CARTESIAN_POINT ( 'NONE',  ( -16.97683809663752186, 66.05000000001261640, -190.1207434663279514 ) ) ;
#42430=CARTESIAN_POINT ( 'NONE',  ( -12.93407622233968901, 66.58221053306039039, -188.1657229405475675 ) ) ;
#42728=VERTEX_POINT ( 'NONE', #79407 ) ;
#42952=LINE ( 'NONE', #45515, #248695 ) ;
#43093=CARTESIAN_POINT ( 'NONE',  ( 13.12229106158775060, 66.56936289831581632, -185.2548468664635379 ) ) ;
#43168=CARTESIAN_POINT ( 'NONE',  ( -21.65000000000000213, 66.05000000001261640, -190.7731074845244166 ) ) ;
#43283=LINE ( 'NONE', #67971, #149841 ) ;
#43366=ORIENTED_EDGE ( 'NONE', *, *, #71773, .T. ) ;
#43367=PRESENTATION_STYLE_ASSIGNMENT (( #143733 ) ) ;
#43494=DIRECTION ( 'NONE',  ( 0.000000000000000000, -6.982962677686266711E-15, 1.000000000000000000 ) ) ;
#43557=DIRECTION ( 'NONE',  ( 0.000000000000000000, 6.982962677686266711E-15, -1.000000000000000000 ) ) ;
#43610=LINE ( 'NONE', #126994, #8305 ) ;
#43732=CARTESIAN_POINT ( 'NONE',  ( -17.27223548799954145, 65.65460260868350417, -181.3895013053292473 ) ) ;
#43788=EDGE_LOOP ( 'NONE', ( #118677, #243564, #11003 ) ) ;
#43821=CARTESIAN_POINT ( 'NONE',  ( -33.72168855820451938, 66.05000000001254534, -182.6731074845243654 ) ) ;
#43947=AXIS2_PLACEMENT_3D ( 'NONE', #236778, #59397, #219784 ) ;
#44042=FACE_OUTER_BOUND ( 'NONE', #253873, .T. ) ;
#44234=DIRECTION ( 'NONE',  ( -0.000000000000000000, -6.982962677686266711E-15, 1.000000000000000000 ) ) ;
#44330=CARTESIAN_POINT ( 'NONE',  ( -16.86337532320261090, 66.02003279578819672, -182.5741830155416210 ) ) ;
#44383=CARTESIAN_POINT ( 'NONE',  ( 15.07585980824111793, 66.58236703690626257, -185.3741590187921418 ) ) ;
#44386=ADVANCED_FACE ( 'NONE', ( #163838 ), #64726, .F. ) ;
#44392=AXIS2_PLACEMENT_3D ( 'NONE', #9493, #89026, #168634 ) ;
#44608=CYLINDRICAL_SURFACE ( 'NONE', #205533, 0.09999999999998898659 ) ;
#44637=CARTESIAN_POINT ( 'NONE',  ( 20.04999999999999716, 67.25000000001260503, -194.2731074845244166 ) ) ;
#44816=CARTESIAN_POINT ( 'NONE',  ( -17.29158576265543346, 65.63525233399461456, -181.4403492397322566 ) ) ;
#44963=CARTESIAN_POINT ( 'NONE',  ( -16.94107738177415712, 65.98576071487597972, -190.9731074845244336 ) ) ;
#45046=CYLINDRICAL_SURFACE ( 'NONE', #106887, 0.09999999999999939493 ) ;
#45187=DIRECTION ( 'NONE',  ( 1.000000000000000000, 0.000000000000000000, 0.000000000000000000 ) ) ;
#45497=VERTEX_POINT ( 'NONE', #30998 ) ;
#45515=CARTESIAN_POINT ( 'NONE',  ( -21.65000000000000213, 65.95000000001255103, -182.6731074845244223 ) ) ;
#45577=ADVANCED_FACE ( 'NONE', ( #191121 ), #245942, .F. ) ;
#45616=CARTESIAN_POINT ( 'NONE',  ( -15.75000000000000355, 66.15000000001258229, -186.7731074845244166 ) ) ;
#45658=CARTESIAN_POINT ( 'NONE',  ( 12.48201962039797763, 66.62334006147904120, -185.8949149363072024 ) ) ;
#45891=CIRCLE ( 'NONE', #108258, 0.09999999999998898659 ) ;
#45915=DIRECTION ( 'NONE',  ( -1.000000000000000000, 0.000000000000000000, 0.000000000000000000 ) ) ;
#46192=CARTESIAN_POINT ( 'NONE',  ( -23.25000000000000355, 66.05000000001264482, -194.2731074845244166 ) ) ;
#46210=CARTESIAN_POINT ( 'NONE',  ( -16.84793658983456410, 66.05000000001253113, -182.7567541623338627 ) ) ;
#46241=ORIENTED_EDGE ( 'NONE', *, *, #255913, .F. ) ;
#46407=DIRECTION ( 'NONE',  ( 1.020425574104004196E-15, 6.982962677686266711E-15, -1.000000000000000000 ) ) ;
#46517=ORIENTED_EDGE ( 'NONE', *, *, #145313, .T. ) ;
#46586=ORIENTED_EDGE ( 'NONE', *, *, #70916, .T. ) ;
#47067=CARTESIAN_POINT ( 'NONE',  ( -16.87683809663752399, 66.15000000001262492, -190.1207434663279514 ) ) ;
#47302=ADVANCED_FACE ( 'NONE', ( #242787 ), #44608, .T. ) ;
#47477=VERTEX_POINT ( 'NONE', #148848 ) ;
#47486=DIRECTION ( 'NONE',  ( 1.020425574104004196E-15, -6.982962677686266711E-15, 1.000000000000000000 ) ) ;
#47550=EDGE_CURVE ( 'NONE', #194460, #243580, #57415, .T. ) ;
#47643=CARTESIAN_POINT ( 'NONE',  ( -17.01825945287481545, 66.05000000001255955, -182.7731074845244450 ) ) ;
#47791=CARTESIAN_POINT ( 'NONE',  ( -16.77977881697926321, 66.05339806647970136, -190.8617289114093865 ) ) ;
#47886=ADVANCED_FACE ( 'NONE', ( #171643 ), #176757, .F. ) ;
#48296=AXIS2_PLACEMENT_3D ( 'NONE', #62391, #63662, #101461 ) ;
#48324=CARTESIAN_POINT ( 'NONE',  ( -20.65000000000000568, 70.35000000001264198, -194.2731074845243882 ) ) ;
#48332=CARTESIAN_POINT ( 'NONE',  ( -18.40000000000000213, 64.25000000001253397, -179.2731074845244450 ) ) ;
#48366=DIRECTION ( 'NONE',  ( 0.000000000000000000, 1.000000000000000000, 0.000000000000000000 ) ) ;
#48684=CARTESIAN_POINT ( 'NONE',  ( -23.25000000000000355, 70.35000000001255671, -182.6731074845243938 ) ) ;
#48783=CARTESIAN_POINT ( 'NONE',  ( -16.87683809663752399, 66.15000000001255387, -183.4254715027207396 ) ) ;
#48918=EDGE_LOOP ( 'NONE', ( #165666, #30005 ) ) ;
#49183=VERTEX_POINT ( 'NONE', #48684 ) ;
#49357=PRODUCT ( 'Snap Open Cable Crossbars 11', 'Snap Open Cable Crossbars 11', '', ( #173516 ) ) ;
#49752=DIRECTION ( 'NONE',  ( -1.000000000000000000, 0.000000000000000000, -0.000000000000000000 ) ) ;
#50210=CARTESIAN_POINT ( 'NONE',  ( -20.65000000000000568, 68.75000000001263345, -194.2731074845244166 ) ) ;
#50353=CARTESIAN_POINT ( 'NONE',  ( -16.78055652883087134, 66.05322308388724650, -190.8623156469320179 ) ) ;
#50528=CARTESIAN_POINT ( 'NONE',  ( -16.81453046979149590, 66.06089771857169524, -190.8113809609214115 ) ) ;
#50636=DIRECTION ( 'NONE',  ( 1.000000000000000000, 0.000000000000000000, 0.000000000000000000 ) ) ;
#50644=CIRCLE ( 'NONE', #225431, 0.09999999999999105438 ) ;
#50788=CARTESIAN_POINT ( 'NONE',  ( -18.40000000000000213, 64.51332499825495859, -194.2731074845244450 ) ) ;
#50906=CARTESIAN_POINT ( 'NONE',  ( -16.93710578446424009, 66.05000000001261640, -190.6043035007245408 ) ) ;
#51220=ORIENTED_EDGE ( 'NONE', *, *, #124749, .F. ) ;
#51225=ORIENTED_EDGE ( 'NONE', *, *, #88365, .T. ) ;
#51540=CARTESIAN_POINT ( 'NONE',  ( -17.73285935862584495, 65.14201819622915934, -193.2816692942934651 ) ) ;
#51636=B_SPLINE_CURVE_WITH_KNOTS ( 'NONE', 3,
 ( #238254, #154909, #235687, #55738, #256477, #233160, #135296 ),
 .UNSPECIFIED., .F., .F.,
 ( 4, 3, 4 ),
 ( 0.000000000000000000, 4.520325912680430423E-05, 5.794988040901246848E-05 ),
 .UNSPECIFIED. ) ;
#51684=AXIS2_PLACEMENT_3D ( 'NONE', #221669, #143433, #122613 ) ;
#51750=ORIENTED_EDGE ( 'NONE', *, *, #111064, .F. ) ;
#52072=LINE ( 'NONE', #131624, #257704 ) ;
#52143=CARTESIAN_POINT ( 'NONE',  ( -16.85939681242905763, 66.09477481408723065, -182.9831855293329852 ) ) ;
#52207=CARTESIAN_POINT ( 'NONE',  ( -21.64999999999999858, 65.95000000001255103, -182.7731074845244450 ) ) ;
#52378=( BOUNDED_CURVE ( )  B_SPLINE_CURVE ( 3, ( #199720, #83564, #163152, #144843 ),
 .UNSPECIFIED., .F., .F. ) 
 B_SPLINE_CURVE_WITH_KNOTS ( ( 4, 4 ),
 ( 5.731445031868798168, 5.983100554402348337 ),
 .UNSPECIFIED. ) 
 CURVE ( )  GEOMETRIC_REPRESENTATION_ITEM ( )  RATIONAL_B_SPLINE_CURVE ( ( 1.000000000000000000, 0.9947294176030464508, 0.9947294176030464508, 1.000000000000000000 ) ) 
 REPRESENTATION_ITEM ( '' )  );
#52482=STYLED_ITEM ( 'NONE', ( #31988 ), #237827 ) ;
#52594=CARTESIAN_POINT ( 'NONE',  ( -16.87487986503753845, 66.04999244492699972, -190.8731327448377044 ) ) ;
#52729=CARTESIAN_POINT ( 'NONE',  ( -18.40000000000000213, 64.25000000001261924, -190.8731074845244393 ) ) ;
#52847=CARTESIAN_POINT ( 'NONE',  ( -18.41431012584568450, 64.51252797080444168, -194.2963434976261112 ) ) ;
#52940=CARTESIAN_POINT ( 'NONE',  ( -16.81095280782811230, 66.05000000001261640, -190.8731074845252920 ) ) ;
#53088=ORIENTED_EDGE ( 'NONE', *, *, #79263, .T. ) ;
#53342=EDGE_CURVE ( 'NONE', #18319, #127125, #160883, .T. ) ;
#53376=CARTESIAN_POINT ( 'NONE',  ( -16.93211319090181632, 66.00001321885507366, -182.6006019852513589 ) ) ;
#53448=CARTESIAN_POINT ( 'NONE',  ( -16.80469485234340965, 66.05784833687151547, -182.7131406405933092 ) ) ;
#53463=ORIENTED_EDGE ( 'NONE', *, *, #29260, .T. ) ;
#53478=CIRCLE ( 'NONE', #236609, 0.09999999999999105438 ) ;
#53482=CARTESIAN_POINT ( 'NONE',  ( 20.04999999999999716, 67.25000000001251976, -182.6731074845244223 ) ) ;
#53508=CARTESIAN_POINT ( 'NONE',  ( -16.79270642812251069, 66.05375578307388196, -190.8620407630891123 ) ) ;
#53591=EDGE_CURVE ( 'NONE', #213303, #147103, #109014, .T. ) ;
#53593=VECTOR ( 'NONE', #169229, 1000.000000000000000 ) ;
#53639=PRODUCT_DEFINITION_SHAPE ( 'NONE', 'NONE',  #144083 ) ;
#53758=CARTESIAN_POINT ( 'NONE',  ( -17.11825945287482753, 65.95000000001260787, -190.7731074845244166 ) ) ;
#53820=DIRECTION ( 'NONE',  ( -1.186688945009010077E-16, -1.000000000000000000, -7.759275652592821052E-15 ) ) ;
#53975=AXIS2_PLACEMENT_3D ( 'NONE', #141031, #41944, #200999 ) ;
#54689=VERTEX_POINT ( 'NONE', #217979 ) ;
#54721=CYLINDRICAL_SURFACE ( 'NONE', #34337, 14.30833333333333890 ) ;
#54771=VERTEX_POINT ( 'NONE', #175082 ) ;
#54831=AXIS2_PLACEMENT_3D ( 'NONE', #86142, #146141, #206128 ) ;
#54961=ORIENTED_EDGE ( 'NONE', *, *, #210, .T. ) ;
#54994=EDGE_CURVE ( 'NONE', #120323, #85330, #9225, .T. ) ;
#55140=ORIENTED_EDGE ( 'NONE', *, *, #215031, .T. ) ;
#55219=ORIENTED_EDGE ( 'NONE', *, *, #67633, .F. ) ;
#55342=DIRECTION ( 'NONE',  ( 0.2834754621636358940, 0.2834754621636501049, -0.9161240771326873977 ) ) ;
#55652=CIRCLE ( 'NONE', #243127, 0.09999999999999939493 ) ;
#55738=CARTESIAN_POINT ( 'NONE',  ( -18.35663730107557257, 64.52609257350141547, -194.2731074845244450 ) ) ;
#55914=ORIENTED_EDGE ( 'NONE', *, *, #79742, .F. ) ;
#56061=ORIENTED_EDGE ( 'NONE', *, *, #258026, .T. ) ;
#56115=CARTESIAN_POINT ( 'NONE',  ( 15.74999999999999645, 66.15000000001258229, -186.7731074845244450 ) ) ;
#56139=PLANE ( 'NONE',  #143198 ) ;
#56324=CARTESIAN_POINT ( 'NONE',  ( -16.87036670365548474, 66.01058118071090064, -182.5435473672224020 ) ) ;
#56395=LINE ( 'NONE', #215482, #113559 ) ;
#56464=AXIS2_PLACEMENT_3D ( 'NONE', #167235, #129357, #30276 ) ;
#56501=CARTESIAN_POINT ( 'NONE',  ( -16.94445028196808778, 66.00793639031486748, -190.9157773061059800 ) ) ;
#56554=MECHANICAL_DESIGN_GEOMETRIC_PRESENTATION_REPRESENTATION('',(#52482),#164920);
#56753=CARTESIAN_POINT ( 'NONE',  ( -17.71734398241073549, 65.15764277154798378, -180.2979692315188345 ) ) ;
#56893=EDGE_LOOP ( 'NONE', ( #101737, #51750, #57218, #158533 ) ) ;
#57082=DIRECTION ( 'NONE',  ( -1.073024830501117725E-15, -6.982962677686266711E-15, 1.000000000000000000 ) ) ;
#57218=ORIENTED_EDGE ( 'NONE', *, *, #53591, .F. ) ;
#57415=LINE ( 'NONE', #196935, #126627 ) ;
#57487=ORIENTED_EDGE ( 'NONE', *, *, #241067, .T. ) ;
#57650=CARTESIAN_POINT ( 'NONE',  ( -16.89081410710458542, 66.04868147016543389, -182.6687015646880639 ) ) ;
#57799=EDGE_CURVE ( 'NONE', #213303, #42728, #34256, .T. ) ;
#57844=ORIENTED_EDGE ( 'NONE', *, *, #153022, .F. ) ;
#57906=CARTESIAN_POINT ( 'NONE',  ( -16.94275863009466576, 66.01050395135021631, -190.9148048665655324 ) ) ;
#58153=CIRCLE ( 'NONE', #158192, 0.5000000000000004441 ) ;
#58164=CARTESIAN_POINT ( 'NONE',  ( 20.27550659511089037, 66.78395627750369101, -182.6731074845244223 ) ) ;
#58794=ORIENTED_EDGE ( 'NONE', *, *, #112790, .F. ) ;
#58919=CARTESIAN_POINT ( 'NONE',  ( -16.87665923198281348, 66.05000000001255955, -182.6731074845244223 ) ) ;
#59263=VECTOR ( 'NONE', #154551, 1000.000000000000000 ) ;
#59331=CARTESIAN_POINT ( 'NONE',  ( -16.94878442675510399, 66.00827089702154638, -182.6348879088865829 ) ) ;
#59380=CARTESIAN_POINT ( 'NONE',  ( -16.81744102076749314, 66.05000000001261640, -190.8731074845244393 ) ) ;
#59397=DIRECTION ( 'NONE',  ( 1.073024830501117725E-15, 6.982962677686266711E-15, -1.000000000000000000 ) ) ;
#59425=EDGE_LOOP ( 'NONE', ( #92137, #203479, #41376 ) ) ;
#59623=ORIENTED_EDGE ( 'NONE', *, *, #60027, .T. ) ;
#59879=( LENGTH_UNIT ( ) NAMED_UNIT ( * ) SI_UNIT ( .MILLI., .METRE. ) );
#60027=EDGE_CURVE ( 'NONE', #63287, #157258, #28039, .T. ) ;
#60072=CARTESIAN_POINT ( 'NONE',  ( 15.73863059295127442, 66.64859682587091072, -186.5435770476858579 ) ) ;
#60074=ORIENTED_EDGE ( 'NONE', *, *, #54994, .F. ) ;
#60161=AXIS2_PLACEMENT_3D ( 'NONE', #196294, #138855, #254926 ) ;
#60227=CARTESIAN_POINT ( 'NONE',  ( -16.87331047859649757, 66.05000000001255955, -182.6731074845244223 ) ) ;
#60296=CARTESIAN_POINT ( 'NONE',  ( 12.29592348164038818, 66.64419340838244921, -187.2320049529782864 ) ) ;
#60342=CARTESIAN_POINT ( 'NONE',  ( -18.40000000000000213, 64.52683809665005299, -182.5731074845244279 ) ) ;
#60367=CARTESIAN_POINT ( 'NONE',  ( -16.93226657140833069, 66.00045617728818570, -190.9443943735508071 ) ) ;
#60522=CARTESIAN_POINT ( 'NONE',  ( -20.65000000000000568, 68.75000000001256240, -182.6731074845244223 ) ) ;
#60625=DIRECTION ( 'NONE',  ( 0.000000000000000000, 1.000000000000000000, 6.982962677686266711E-15 ) ) ;
#60634=CARTESIAN_POINT ( 'NONE',  ( -16.86445178670600598, 66.03778837089669196, -182.6323300464076453 ) ) ;
#60706=CARTESIAN_POINT ( 'NONE',  ( -17.29838795457914102, 65.62845014207091765, -181.4183662019063377 ) ) ;
#60767=VERTEX_POINT ( 'NONE', #121894 ) ;
#60920=CARTESIAN_POINT ( 'NONE',  ( -21.64999999999999858, 65.95000000001262208, -190.8731074845244393 ) ) ;
#60924=ORIENTED_EDGE ( 'NONE', *, *, #226458, .F. ) ;
#61160=DIRECTION ( 'NONE',  ( -0.000000000000000000, -6.982962677686266711E-15, 1.000000000000000000 ) ) ;
#61262=VECTOR ( 'NONE', #101782, 1000.000000000000000 ) ;
#61264=ORIENTED_EDGE ( 'NONE', *, *, #242148, .F. ) ;
#61304=EDGE_LOOP ( 'NONE', ( #125214, #79659, #9365, #51225 ) ) ;
#61311=CARTESIAN_POINT ( 'NONE',  ( -14.00000000000000178, 66.15000000001258229, -186.7731074845244166 ) ) ;
#61337=PLANE ( 'NONE',  #80339 ) ;
#61364=CARTESIAN_POINT ( 'NONE',  ( 14.45963434102923451, 66.54845833862704296, -185.0692319856938184 ) ) ;
#61472=ADVANCED_FACE ( 'NONE', ( #238305 ), #196613, .F. ) ;
#61638=SURFACE_STYLE_FILL_AREA ( #165899 ) ;
#61749=CARTESIAN_POINT ( 'NONE',  ( 15.74999999999999645, 66.15000000001258229, -186.7731074845244450 ) ) ;
#61936=CARTESIAN_POINT ( 'NONE',  ( 18.54999999999999716, 67.25000000001259082, -194.2731074845244166 ) ) ;
#61947=CARTESIAN_POINT ( 'NONE',  ( -16.92778301347286529, 65.99905508317719693, -182.5945893765574795 ) ) ;
#62008=CARTESIAN_POINT ( 'NONE',  ( -15.15766958671844122, 66.58946139148370946, -188.0904194873835422 ) ) ;
#62391=CARTESIAN_POINT ( 'NONE',  ( -23.25000000000000355, 65.95000000001260787, -190.7731074845244166 ) ) ;
#62454=EDGE_CURVE ( 'NONE', #85330, #18319, #202519, .T. ) ;
#62570=EDGE_LOOP ( 'NONE', ( #79022, #191964, #15887, #171427 ) ) ;
#62662=CARTESIAN_POINT ( 'NONE',  ( 13.43663047529819998, 66.55335465531732098, -185.1123010284242412 ) ) ;
#62779=ADVANCED_FACE ( 'NONE', ( #241276 ), #142149, .F. ) ;
#62784=ADVANCED_FACE ( 'NONE', ( #39232 ), #61337, .T. ) ;
#63028=CARTESIAN_POINT ( 'NONE',  ( 15.48841904831874849, 67.43841904833132617, -182.6731074845244223 ) ) ;
#63037=DIRECTION ( 'NONE',  ( 1.000000000000000000, 0.000000000000000000, 0.000000000000000000 ) ) ;
#63111=( BOUNDED_CURVE ( )  B_SPLINE_CURVE ( 3, ( #78896, #178045, #56753, #176758 ),
 .UNSPECIFIED., .F., .F. ) 
 B_SPLINE_CURVE_WITH_KNOTS ( ( 4, 4 ),
 ( 0.3000847527772375622, 0.5517402753107888413 ),
 .UNSPECIFIED. ) 
 CURVE ( )  GEOMETRIC_REPRESENTATION_ITEM ( )  RATIONAL_B_SPLINE_CURVE ( ( 1.000000000000000000, 0.9947294176030464508, 0.9947294176030464508, 1.000000000000000000 ) ) 
 REPRESENTATION_ITEM ( '' )  );
#63193=CARTESIAN_POINT ( 'NONE',  ( -16.87401514999228169, 66.05000000001255955, -182.7430894919923219 ) ) ;
#63269=CARTESIAN_POINT ( 'NONE',  ( -14.87779219673431008, 66.56936653093978862, -188.2913416897003174 ) ) ;
#63287=VERTEX_POINT ( 'NONE', #110085 ) ;
#63430=CARTESIAN_POINT ( 'NONE',  ( -21.65000000000000213, 66.05000000001261640, -190.8731074845244393 ) ) ;
#63464=CARTESIAN_POINT ( 'NONE',  ( 20.27550659511088682, 66.78395627750377628, -194.2731074845244166 ) ) ;
#63631=CIRCLE ( 'NONE', #155450, 14.30833333333333890 ) ;
#63662=DIRECTION ( 'NONE',  ( 1.000000000000000000, 0.000000000000000000, 0.000000000000000000 ) ) ;
#63746=B_SPLINE_CURVE_WITH_KNOTS ( 'NONE', 3,
 ( #181949, #142788, #65840, #82801, #204062, #62008, #162396, #63269, #25450, #146643, #145375, #104931, #41178, #224901, #184494, #125811, #222318, #120713, #221056, #42430, #202786, #71012, #33188, #190960, #167544, #129672 ),
 .UNSPECIFIED., .F., .F.,
 ( 4, 2, 2, 2, 2, 2, 2, 2, 2, 2, 2, 2, 4 ),
 ( 0.005476422646581329164, 0.006160811967703526230, 0.006845201288825725032, 0.007187395949386824433, 0.007529590609947924701, 0.007871785270509024102, 0.008213979931070123502, 0.008556174591631222903, 0.008898369252192322304, 0.009240563912753421705, 0.009582758573314522840, 0.01026714789443678236, 0.01095153721555904361 ),
 .UNSPECIFIED. ) ;
#63843=CARTESIAN_POINT ( 'NONE',  ( -16.97683809663752186, 66.05000000001257376, -183.4254715027207681 ) ) ;
#63919=VECTOR ( 'NONE', #167636, 1000.000000000000000 ) ;
#63937=CARTESIAN_POINT ( 'NONE',  ( 15.31784899511109010, 66.60336962369487424, -185.6160500917061995 ) ) ;
#64129=CARTESIAN_POINT ( 'NONE',  ( -13.54036565897074773, 66.54845833862705717, -185.0692319856938468 ) ) ;
#64167=CARTESIAN_POINT ( 'NONE',  ( -23.25000000000000355, 65.95000000001255103, -182.7731074845244450 ) ) ;
#64251=EDGE_CURVE ( 'NONE', #104788, #75549, #18640, .T. ) ;
#64726=PLANE ( 'NONE',  #246356 ) ;
#64743=CARTESIAN_POINT ( 'NONE',  ( 20.27550659511089037, 66.78395627750374786, -190.8731074845244393 ) ) ;
#65289=LINE ( 'NONE', #43168, #74326 ) ;
#65385=VECTOR ( 'NONE', #176570, 999.9999999999998863 ) ;
#65404=CARTESIAN_POINT ( 'NONE',  ( -15.69373346032658034, 66.64320997496669463, -186.3182809759104543 ) ) ;
#65409=VECTOR ( 'NONE', #28818, 1000.000000000000000 ) ;
#65434=ORIENTED_EDGE ( 'NONE', *, *, #160897, .F. ) ;
#65503=PRODUCT_DEFINITION_FORMATION_WITH_SPECIFIED_SOURCE ( 'ANY', '', #49357, .NOT_KNOWN. ) ;
#65597=ORIENTED_EDGE ( 'NONE', *, *, #214438, .T. ) ;
#65782=CARTESIAN_POINT ( 'NONE',  ( -16.96982749440682525, 66.05000000001255955, -183.1478858933352001 ) ) ;
#65785=LINE ( 'NONE', #107479, #107561 ) ;
#65797=ORIENTED_EDGE ( 'NONE', *, *, #256856, .T. ) ;
#65815=ORIENTED_EDGE ( 'NONE', *, *, #145774, .F. ) ;
#65840=CARTESIAN_POINT ( 'NONE',  ( -15.70407651835961005, 66.64419340838244921, -187.2320049529782011 ) ) ;
#66216=CARTESIAN_POINT ( 'NONE',  ( -21.65000000000000213, 68.75000000001263345, -194.2731074845244166 ) ) ;
#66225=LINE ( 'NONE', #149631, #102001 ) ;
#66269=VECTOR ( 'NONE', #155486, 1000.000000000000000 ) ;
#66663=CARTESIAN_POINT ( 'NONE',  ( -16.94445028196807002, 66.00793639031481064, -182.6304376629428816 ) ) ;
#67072=CARTESIAN_POINT ( 'NONE',  ( -16.82055514392354567, 66.05000000001255955, -182.6999055590671048 ) ) ;
#67633=EDGE_CURVE ( 'NONE', #13472, #201172, #223626, .T. ) ;
#67687=CARTESIAN_POINT ( 'NONE',  ( -16.90138253750126651, 66.05000000001254534, -182.8115447766198827 ) ) ;
#67702=CARTESIAN_POINT ( 'NONE',  ( -23.25000000000000355, 64.25000000001261924, -190.8731074845244393 ) ) ;
#67732=CARTESIAN_POINT ( 'NONE',  ( -16.86420534634261514, 66.02938455442082955, -182.6047709352870356 ) ) ;
#67748=VECTOR ( 'NONE', #217334, 1000.000000000000000 ) ;
#67781=CARTESIAN_POINT ( 'NONE',  ( 12.25000000000000355, 66.65000000001256808, -186.6588398769083028 ) ) ;
#67839=VERTEX_POINT ( 'NONE', #252083 ) ;
#67890=EDGE_CURVE ( 'NONE', #92187, #2878, #176428, .T. ) ;
#67906=ORIENTED_EDGE ( 'NONE', *, *, #173222, .T. ) ;
#67931=CARTESIAN_POINT ( 'NONE',  ( -16.92280123533723568, 66.05000000001261640, -190.6724751704383323 ) ) ;
#67956=LINE ( 'NONE', #185341, #176819 ) ;
#67971=CARTESIAN_POINT ( 'NONE',  ( -33.72168855820451938, 66.05000000001260219, -190.8731074845244962 ) ) ;
#68212=ORIENTED_EDGE ( 'NONE', *, *, #180707, .T. ) ;
#68361=FACE_OUTER_BOUND ( 'NONE', #33652, .T. ) ;
#68472=LINE ( 'NONE', #253507, #65385 ) ;
#68976=EDGE_CURVE ( 'NONE', #71999, #131991, #225710, .T. ) ;
#69038=CARTESIAN_POINT ( 'NONE',  ( -17.01473183483379970, 66.05000000001255955, -182.7731074845244734 ) ) ;
#69313=VECTOR ( 'NONE', #120915, 999.9999999999998863 ) ;
#69361=CARTESIAN_POINT ( 'NONE',  ( -16.94107738177415712, 65.98576071487597972, -190.9731074845244336 ) ) ;
#69467=VECTOR ( 'NONE', #94231, 1000.000000000000000 ) ;
#69693=CARTESIAN_POINT ( 'NONE',  ( -16.86757978335472075, 66.03434962097831828, -190.9251028313569236 ) ) ;
#69906=ORIENTED_EDGE ( 'NONE', *, *, #146910, .T. ) ;
#69954=EDGE_CURVE ( 'NONE', #131991, #160738, #157596, .T. ) ;
#69979=ORIENTED_EDGE ( 'NONE', *, *, #145774, .T. ) ;
#69981=CARTESIAN_POINT ( 'NONE',  ( -16.77732147262506146, 66.05403306739390246, -182.6866162412485437 ) ) ;
#70180=ORIENTED_EDGE ( 'NONE', *, *, #69954, .F. ) ;
#70257=PLANE ( 'NONE',  #197830 ) ;
#70309=DIRECTION ( 'NONE',  ( 1.000000000000000000, -1.646408749285562060E-14, -1.073024830501232702E-15 ) ) ;
#70467=CARTESIAN_POINT ( 'NONE',  ( -14.00000000000000178, 66.15000000001258229, -186.7731074845244166 ) ) ;
#70708=( BOUNDED_SURFACE ( )  B_SPLINE_SURFACE ( 3, 2, ( 
 ( #18948, #137599, #239299 ),
 ( #180609, #179342, #61947 ),
 ( #60634, #98449, #123202 ),
 ( #202730, #159766, #59331 ) ),
 .UNSPECIFIED., .F., .F., .F. ) 
 B_SPLINE_SURFACE_WITH_KNOTS ( ( 4, 4 ),
 ( 3, 3 ),
 ( 0.0008258556059633768206, 0.0009616864997632988948 ),
 ( 0.000000000000000000, 1.000000000000000000 ),
 .UNSPECIFIED. ) 
 GEOMETRIC_REPRESENTATION_ITEM ( )  RATIONAL_B_SPLINE_SURFACE ( (
 ( 1.000000000000000000, 0.9152888060719411856, 1.000000000000000000),
 ( 1.000000000000000000, 0.9327727094137941988, 1.000000000000000000),
 ( 1.000000000000000000, 0.9369023509258418425, 1.000000000000000000),
 ( 1.000000000000000000, 0.9246339933864583527, 1.000000000000000000) ) ) 
 REPRESENTATION_ITEM ( '' )  SURFACE ( )  );
#70737=VERTEX_POINT ( 'NONE', #225854 ) ;
#70916=EDGE_CURVE ( 'NONE', #197652, #228950, #135759, .T. ) ;
#71012=CARTESIAN_POINT ( 'NONE',  ( -12.60206096961793776, 66.61031399435691469, -187.8502639781731034 ) ) ;
#71423=CARTESIAN_POINT ( 'NONE',  ( -16.80100426158790228, 66.05684947961644582, -190.8401617316903582 ) ) ;
#71495=AXIS2_PLACEMENT_3D ( 'NONE', #220907, #102221, #36602 ) ;
#71663=ORIENTED_EDGE ( 'NONE', *, *, #11425, .F. ) ;
#71715=ORIENTED_EDGE ( 'NONE', *, *, #160734, .T. ) ;
#71773=EDGE_CURVE ( 'NONE', #130997, #157258, #236479, .T. ) ;
#71848=CARTESIAN_POINT ( 'NONE',  ( -16.97683809663752186, 66.05000000001264482, -194.2731074845244166 ) ) ;
#71978=AXIS2_PLACEMENT_3D ( 'NONE', #217346, #161261, #221201 ) ;
#71999=VERTEX_POINT ( 'NONE', #229757 ) ;
#72007=CARTESIAN_POINT ( 'NONE',  ( 16.87683809663749557, 66.05000000001257376, -182.6731074845244223 ) ) ;
#72073=LINE ( 'NONE', #169923, #76979 ) ;
#72135=ADVANCED_FACE ( 'NONE', ( #217870 ), #174973, .T. ) ;
#72204=CIRCLE ( 'NONE', #188697, 1.749999999999998002 ) ;
#72440=AXIS2_PLACEMENT_3D ( 'NONE', #147209, #170680, #127654 ) ;
#72553=CARTESIAN_POINT ( 'NONE',  ( -16.97683809663752186, 66.15000000001255387, -183.4254715027207396 ) ) ;
#72611=CARTESIAN_POINT ( 'NONE',  ( -18.40000000000000213, 64.25000000001256240, -182.6731074845244507 ) ) ;
#72666=ADVANCED_FACE ( 'NONE', ( #85415 ), #45046, .F. ) ;
#72844=VECTOR ( 'NONE', #153775, 1000.000000000000000 ) ;
#72900=CARTESIAN_POINT ( 'NONE',  ( 13.99999999999999822, 66.15000000001258229, -186.7731074845244450 ) ) ;
#72904=EDGE_CURVE ( 'NONE', #67839, #86769, #68472, .T. ) ;
#72956=EDGE_CURVE ( 'NONE', #49183, #79239, #136108, .T. ) ;
#73216=VERTEX_POINT ( 'NONE', #38050 ) ;
#73906=LINE ( 'NONE', #72611, #172787 ) ;
#74009=CARTESIAN_POINT ( 'NONE',  ( -16.85312841634287651, 66.08639382269238638, -190.6259343512319049 ) ) ;
#74091=VERTEX_POINT ( 'NONE', #220845 ) ;
#74093=EDGE_CURVE ( 'NONE', #188385, #154893, #53478, .T. ) ;
#74326=VECTOR ( 'NONE', #223074, 1000.000000000000000 ) ;
#74395=CARTESIAN_POINT ( 'NONE',  ( -16.82542659449972788, 66.06550010858516941, -190.7784718844984013 ) ) ;
#74558=VERTEX_POINT ( 'NONE', #206267 ) ;
#74667=LINE ( 'NONE', #177609, #86696 ) ;
#74804=EDGE_CURVE ( 'NONE', #24375, #195865, #83014, .T. ) ;
#74854=ORIENTED_EDGE ( 'NONE', *, *, #129599, .T. ) ;
#75319=ORIENTED_EDGE ( 'NONE', *, *, #138324, .T. ) ;
#75325=DIRECTION ( 'NONE',  ( 0.7071067811865487940, -0.7071067811865462405, -4.216150419019403701E-15 ) ) ;
#75503=CARTESIAN_POINT ( 'NONE',  ( -16.97683809663752186, 66.15000000001261071, -190.1207434663279514 ) ) ;
#75549=VERTEX_POINT ( 'NONE', #120382 ) ;
#75663=CARTESIAN_POINT ( 'NONE',  ( -16.84793658983408449, 66.05000000001261640, -190.7894608067139472 ) ) ;
#75787=VERTEX_POINT ( 'NONE', #173657 ) ;
#76104=VERTEX_POINT ( 'NONE', #182603 ) ;
#76475=VERTEX_POINT ( 'NONE', #148281 ) ;
#76574=CARTESIAN_POINT ( 'NONE',  ( -21.64999999999999858, 66.65000000001255387, -182.6731074845244223 ) ) ;
#76697=ORIENTED_EDGE ( 'NONE', *, *, #175897, .T. ) ;
#76703=CARTESIAN_POINT ( 'NONE',  ( -16.87331047859649757, 66.05000000001255955, -182.6731074845244223 ) ) ;
#76765=ORIENTED_EDGE ( 'NONE', *, *, #2026, .T. ) ;
#76871=CARTESIAN_POINT ( 'NONE',  ( -20.65000000000000568, 68.75000000001263345, -194.2731074845244166 ) ) ;
#76979=VECTOR ( 'NONE', #188160, 1000.000000000000000 ) ;
#77298=EDGE_CURVE ( 'NONE', #81857, #103692, #228410, .T. ) ;
#77357=CARTESIAN_POINT ( 'NONE',  ( -16.93440969289730802, 66.00481482419864676, -190.9318732995136259 ) ) ;
#77659=ORIENTED_EDGE ( 'NONE', *, *, #64251, .F. ) ;
#77887=ORIENTED_EDGE ( 'NONE', *, *, #7434, .T. ) ;
#77905=DIRECTION ( 'NONE',  ( -0.000000000000000000, -6.982962677686266711E-15, 1.000000000000000000 ) ) ;
#78167=VERTEX_POINT ( 'NONE', #18775 ) ;
#78219=DIRECTION ( 'NONE',  ( -1.186688945009010077E-16, -1.000000000000000000, -6.982962677686266711E-15 ) ) ;
#78314=DIRECTION ( 'NONE',  ( 1.186688945009009831E-16, 1.000000000000000000, 6.982962677686266711E-15 ) ) ;
#78343=ORIENTED_EDGE ( 'NONE', *, *, #175157, .F. ) ;
#78565=FACE_OUTER_BOUND ( 'NONE', #43788, .T. ) ;
#78579=CARTESIAN_POINT ( 'NONE',  ( 13.12220780326570768, 66.56936653093980283, -188.2913416897004026 ) ) ;
#78638=CARTESIAN_POINT ( 'NONE',  ( -16.94309007106720699, 66.00777380744260370, -190.9173162019689300 ) ) ;
#78647=ADVANCED_FACE ( 'NONE', ( #245249 ), #147421, .F. ) ;
#78784=ORIENTED_EDGE ( 'NONE', *, *, #149566, .T. ) ;
#78896=CARTESIAN_POINT ( 'NONE',  ( -16.87036670365548474, 66.01058118071090064, -182.5435473672224020 ) ) ;
#79022=ORIENTED_EDGE ( 'NONE', *, *, #160734, .F. ) ;
#79060=ORIENTED_EDGE ( 'NONE', *, *, #67890, .F. ) ;
#79085=CARTESIAN_POINT ( 'NONE',  ( -18.40000000000000213, 64.66825945288736932, -182.6731074845244507 ) ) ;
#79114=LINE ( 'NONE', #6974, #169581 ) ;
#79239=VERTEX_POINT ( 'NONE', #136172 ) ;
#79263=EDGE_CURVE ( 'NONE', #120323, #180338, #11352, .T. ) ;
#79267=ORIENTED_EDGE ( 'NONE', *, *, #67890, .T. ) ;
#79407=CARTESIAN_POINT ( 'NONE',  ( -16.94445028196808778, 66.00793639031486748, -190.9157773061059800 ) ) ;
#79579=EDGE_LOOP ( 'NONE', ( #190941, #94657, #145872, #84165 ) ) ;
#79659=ORIENTED_EDGE ( 'NONE', *, *, #205832, .T. ) ;
#79742=EDGE_CURVE ( 'NONE', #199626, #169837, #217982, .T. ) ;
#79812=CARTESIAN_POINT ( 'NONE',  ( -12.33960340485503870, 66.63925083009745265, -186.2085373439171008 ) ) ;
#79842=CARTESIAN_POINT ( 'NONE',  ( 21.13736287352038445, 67.95335762362863363, -194.2731074845244166 ) ) ;
#79844=CARTESIAN_POINT ( 'NONE',  ( 13.54556439290363024, 66.54940788787888550, -188.4669191657160638 ) ) ;
#79982=CARTESIAN_POINT ( 'NONE',  ( -17.11825945287482753, 65.95000000001262208, -190.8731074845244393 ) ) ;
#80227=EDGE_LOOP ( 'NONE', ( #195749, #204512, #240465, #100653, #235555, #191277, #35762, #248961, #132494 ) ) ;
#80249=CARTESIAN_POINT ( 'NONE',  ( -17.78241384942841208, 65.14442424721221414, -180.2721451569497049 ) ) ;
#80335=DIRECTION ( 'NONE',  ( -0.000000000000000000, -6.982962677686266711E-15, 1.000000000000000000 ) ) ;
#80339=AXIS2_PLACEMENT_3D ( 'NONE', #202133, #78314, #101709 ) ;
#80679=ORIENTED_EDGE ( 'NONE', *, *, #214169, .T. ) ;
#80800=CARTESIAN_POINT ( 'NONE',  ( -17.05016517655715091, 66.05000000001636806, -190.8504094885308575 ) ) ;
#80911=CARTESIAN_POINT ( 'NONE',  ( 15.39170923737818342, 66.61047060254585972, -185.7059995716307981 ) ) ;
#81103=CARTESIAN_POINT ( 'NONE',  ( -14.45422546970482713, 66.54939790392400312, -185.0792115214277089 ) ) ;
#81199=CARTESIAN_POINT ( 'NONE',  ( -16.94037747912386394, 65.98646061752627645, -190.9719765265489286 ) ) ;
#81363=CIRCLE ( 'NONE', #168928, 0.09999999999999939493 ) ;
#81365=CARTESIAN_POINT ( 'NONE',  ( -17.04295772865475200, 65.97510057475101064, -182.6731074845244507 ) ) ;
#81770=AXIS2_PLACEMENT_3D ( 'NONE', #6688, #86200, #247872 ) ;
#81789=ORIENTED_EDGE ( 'NONE', *, *, #212001, .T. ) ;
#81857=VERTEX_POINT ( 'NONE', #154606 ) ;
#82025=FACE_OUTER_BOUND ( 'NONE', #224880, .T. ) ;
#82130=CARTESIAN_POINT ( 'NONE',  ( -16.86578989773640913, 66.01519019875374283, -182.5584425979022285 ) ) ;
#82180=CARTESIAN_POINT ( 'NONE',  ( 15.74999999999999645, 66.65000000001258229, -186.7731074845244166 ) ) ;
#82225=LINE ( 'NONE', #219192, #152853 ) ;
#82371=CARTESIAN_POINT ( 'NONE',  ( -15.57281606413131314, 66.62934494888905590, -185.9972842285434069 ) ) ;
#82559=DIRECTION ( 'NONE',  ( 1.186688945009010077E-16, 1.000000000000000000, 6.982962677686266711E-15 ) ) ;
#82632=DIRECTION ( 'NONE',  ( 0.000000000000000000, -1.000000000000000000, -6.982962677686266711E-15 ) ) ;
#82737=CARTESIAN_POINT ( 'NONE',  ( -16.87998658237729188, 66.05000000001255955, -182.8867470522638143 ) ) ;
#82755=CARTESIAN_POINT ( 'NONE',  ( -17.29158576265543346, 65.63525233399469982, -192.1058657293165766 ) ) ;
#82792=CARTESIAN_POINT ( 'NONE',  ( -16.84421487269769102, 66.05000000001261640, -190.8536053620794632 ) ) ;
#82801=CARTESIAN_POINT ( 'NONE',  ( -15.52965525596988172, 66.62446189796456508, -187.6532316035334702 ) ) ;
#82802=DIRECTION ( 'NONE',  ( 0.000000000000000000, -1.000000000000000000, -6.982962677686266711E-15 ) ) ;
#82804=CARTESIAN_POINT ( 'NONE',  ( -16.90987985657660886, 66.04219248183281366, -182.6538203956407926 ) ) ;
#83014=CIRCLE ( 'NONE', #187131, 1.749999999999999778 ) ;
#83121=DIRECTION ( 'NONE',  ( 1.000000000000000000, 0.000000000000000000, 0.000000000000000000 ) ) ;
#83131=EDGE_CURVE ( 'NONE', #36544, #104788, #63111, .T. ) ;
#83177=ADVANCED_FACE ( 'NONE', ( #217120 ), #239288, .F. ) ;
#83186=EDGE_CURVE ( 'NONE', #5245, #78167, #240569, .T. ) ;
#83276=ADVANCED_FACE ( 'NONE', ( #68361 ), #34996, .F. ) ;
#83564=CARTESIAN_POINT ( 'NONE',  ( -17.71734398241074970, 65.15764277154805484, -193.2482457375300271 ) ) ;
#83745=ORIENTED_EDGE ( 'NONE', *, *, #11076, .T. ) ;
#84165=ORIENTED_EDGE ( 'NONE', *, *, #17235, .F. ) ;
#84401=CARTESIAN_POINT ( 'NONE',  ( -17.11825945287481332, 65.95000000001255103, -182.6731074845244223 ) ) ;
#84438=PLANE ( 'NONE',  #170984 ) ;
#84703=CARTESIAN_POINT ( 'NONE',  ( 18.54999999999999716, 52.34166666667924517, -186.7731074845245303 ) ) ;
#84932=CARTESIAN_POINT ( 'NONE',  ( -12.42749937872396160, 66.62931007840991526, -185.9966423578633510 ) ) ;
#85024=CARTESIAN_POINT ( 'NONE',  ( -23.25000000000000355, 64.25000000001253397, -179.2731074845244450 ) ) ;
#85087=CARTESIAN_POINT ( 'NONE',  ( -16.98495255085916611, 65.99443563401777624, -182.6577246907449421 ) ) ;
#85330=VERTEX_POINT ( 'NONE', #23095 ) ;
#85415=FACE_OUTER_BOUND ( 'NONE', #204158, .T. ) ;
#85562=DIRECTION ( 'NONE',  ( -0.000000000000000000, -6.982962677686266711E-15, 1.000000000000000000 ) ) ;
#85658=FACE_OUTER_BOUND ( 'NONE', #105636, .T. ) ;
#85897=FACE_OUTER_BOUND ( 'NONE', #237099, .T. ) ;
#86109=EDGE_LOOP ( 'NONE', ( #139247, #221133, #241716, #18444 ) ) ;
#86142=CARTESIAN_POINT ( 'NONE',  ( 20.04999999999999716, 67.25000000001257661, -190.8731074845244109 ) ) ;
#86200=DIRECTION ( 'NONE',  ( 0.000000000000000000, 6.982962677686266711E-15, -1.000000000000000000 ) ) ;
#86696=VECTOR ( 'NONE', #154210, 1000.000000000000000 ) ;
#86769=VERTEX_POINT ( 'NONE', #173104 ) ;
#87718=ORIENTED_EDGE ( 'NONE', *, *, #214896, .T. ) ;
#87747=DIRECTION ( 'NONE',  ( 0.000000000000000000, -0.9553114395363127009, 0.2956011730204364252 ) ) ;
#87802=ORIENTED_EDGE ( 'NONE', *, *, #148203, .T. ) ;
#87885=CARTESIAN_POINT ( 'NONE',  ( -16.92280123533733871, 66.05000000001255955, -182.8737397986104725 ) ) ;
#87891=EDGE_CURVE ( 'NONE', #78167, #252512, #206572, .T. ) ;
#88018=ORIENTED_EDGE ( 'NONE', *, *, #145660, .T. ) ;
#88131=CIRCLE ( 'NONE', #54831, 1.500000000000001332 ) ;
#88192=CARTESIAN_POINT ( 'NONE',  ( -16.81744102076749314, 66.05000000001261640, -190.8731074845244393 ) ) ;
#88232=EDGE_LOOP ( 'NONE', ( #206116, #233959 ) ) ;
#88248=ORIENTED_EDGE ( 'NONE', *, *, #114492, .T. ) ;
#88334=ORIENTED_EDGE ( 'NONE', *, *, #114845, .F. ) ;
#88365=EDGE_CURVE ( 'NONE', #54771, #130997, #162237, .T. ) ;
#88551=ADVANCED_FACE ( 'NONE', ( #171251 ), #94493, .T. ) ;
#88736=EDGE_CURVE ( 'NONE', #160738, #100104, #235290, .T. ) ;
#89026=DIRECTION ( 'NONE',  ( 1.000000000000000000, -1.186688945009010077E-16, -8.286604613020808509E-31 ) ) ;
#89094=EDGE_LOOP ( 'NONE', ( #61264, #15789, #100927, #249736, #205503, #124066, #205733, #254720, #153151, #171779, #205861, #159511, #78343, #157974 ) ) ;
#89351=FILL_AREA_STYLE_COLOUR ( '', #169059 ) ;
#89626=ORIENTED_EDGE ( 'NONE', *, *, #22937, .T. ) ;
#89662=CARTESIAN_POINT ( 'NONE',  ( -16.80468759584937644, 66.05784632487846864, -190.8330886183227335 ) ) ;
#90039=CARTESIAN_POINT ( 'NONE',  ( -18.40000000000000213, 64.52683809665003878, -179.2731074845244450 ) ) ;
#90051=CARTESIAN_POINT ( 'NONE',  ( -16.96982749440708815, 66.05000000001261640, -190.3983290757135194 ) ) ;
#90168=CARTESIAN_POINT ( 'NONE',  ( -16.87036670365549895, 66.01058118071094327, -191.0026676018264595 ) ) ;
#90239=ORIENTED_EDGE ( 'NONE', *, *, #145313, .F. ) ;
#90435=ORIENTED_EDGE ( 'NONE', *, *, #53342, .F. ) ;
#90467=CARTESIAN_POINT ( 'NONE',  ( -23.25000000000000355, 64.25000000001264766, -194.2731074845244450 ) ) ;
#90473=( BOUNDED_CURVE ( )  B_SPLINE_CURVE ( 3, ( #129145, #208700, #150011, #130417 ),
 .UNSPECIFIED., .F., .F. ) 
 B_SPLINE_CURVE_WITH_KNOTS ( ( 4, 4 ),
 ( 2.589852378279005496, 2.850972632318389710 ),
 .UNSPECIFIED. ) 
 CURVE ( )  GEOMETRIC_REPRESENTATION_ITEM ( )  RATIONAL_B_SPLINE_CURVE ( ( 1.000000000000000000, 0.9943260843901261525, 0.9943260843901261525, 1.000000000000000000 ) ) 
 REPRESENTATION_ITEM ( '' )  );
#90574=CARTESIAN_POINT ( 'NONE',  ( 21.72449340488909897, 65.71604372252141957, -182.6731074845244223 ) ) ;
#90693=CARTESIAN_POINT ( 'NONE',  ( -16.91256925476571737, 66.01426884188440170, -190.9907499735297165 ) ) ;
#90715=ORIENTED_EDGE ( 'NONE', *, *, #180707, .F. ) ;
#90907=ORIENTED_EDGE ( 'NONE', *, *, #17235, .T. ) ;
#91078=CIRCLE ( 'NONE', #161833, 1.749999999999999778 ) ;
#91130=CARTESIAN_POINT ( 'NONE',  ( 17.23472005113827166, 65.69211804551174794, -181.4765306244557621 ) ) ;
#91350=B_SPLINE_CURVE_WITH_KNOTS ( 'NONE', 3,
 ( #29744, #10151, #152251, #71423, #89662, #50528, #154819, #252591, #34873, #74009, #230479, #169259, #233067, #209629 ),
 .UNSPECIFIED., .F., .F.,
 ( 4, 2, 2, 2, 2, 2, 4 ),
 ( 0.000000000000000000, 2.389617747641766606E-05, 4.779235495283533212E-05, 9.558470990574123225E-05, 0.0001911694198115613131, 0.0003823388396232054050, 0.0007646776792464113522 ),
 .UNSPECIFIED. ) ;
#91490=EDGE_CURVE ( 'NONE', #23645, #166894, #231290, .T. ) ;
#91640=ORIENTED_EDGE ( 'NONE', *, *, #210026, .T. ) ;
#91960=DIRECTION ( 'NONE',  ( 0.000000000000000000, -1.000000000000000000, -6.982962677686266711E-15 ) ) ;
#92126=VECTOR ( 'NONE', #82802, 1000.000000000000000 ) ;
#92137=ORIENTED_EDGE ( 'NONE', *, *, #156087, .T. ) ;
#92187=VERTEX_POINT ( 'NONE', #108796 ) ;
#92266=ORIENTED_EDGE ( 'NONE', *, *, #256768, .T. ) ;
#92324=ORIENTED_EDGE ( 'NONE', *, *, #256990, .F. ) ;
#92948=FACE_OUTER_BOUND ( 'NONE', #164277, .T. ) ;
#92961=PLANE ( 'NONE',  #185454 ) ;
#92993=ORIENTED_EDGE ( 'NONE', *, *, #99944, .T. ) ;
#93250=LINE ( 'NONE', #194946, #221782 ) ;
#93775=CARTESIAN_POINT ( 'NONE',  ( -16.93234230245722216, 66.00189262946545909, -182.6054172028581775 ) ) ;
#93831=DIRECTION ( 'NONE',  ( 0.000000000000000000, 1.000000000000000000, 6.982962677686266711E-15 ) ) ;
#93913=CARTESIAN_POINT ( 'NONE',  ( -16.82055514392402173, 66.05000000001263061, -190.8463094099826378 ) ) ;
#94212=VECTOR ( 'NONE', #168259, 1000.000000000000000 ) ;
#94231=DIRECTION ( 'NONE',  ( -1.000000000000000000, 1.646408749285563322E-14, -1.073024830501002749E-15 ) ) ;
#94243=FACE_OUTER_BOUND ( 'NONE', #152888, .T. ) ;
#94458=FACE_OUTER_BOUND ( 'NONE', #199576, .T. ) ;
#94493=TOROIDAL_SURFACE ( 'NONE', #161149, 14.20833333333334103, 0.1000000000000000056 ) ;
#94657=ORIENTED_EDGE ( 'NONE', *, *, #256990, .T. ) ;
#94951=ORIENTED_EDGE ( 'NONE', *, *, #252223, .T. ) ;
#95116=ORIENTED_EDGE ( 'NONE', *, *, #153700, .F. ) ;
#95165=CARTESIAN_POINT ( 'NONE',  ( 18.39999999999999147, 67.17743825834622839, -194.2731074845244166 ) ) ;
#95640=CARTESIAN_POINT ( 'NONE',  ( -16.94062896051973865, 66.00728089491192918, -190.9205909424056244 ) ) ;
#95790=VERTEX_POINT ( 'NONE', #106775 ) ;
#96302=DIRECTION ( 'NONE',  ( -1.000000000000000000, -1.652117596168391700E-15, -1.153667551319263085E-29 ) ) ;
#96383=LINE ( 'NONE', #194252, #19787 ) ;
#96545=CARTESIAN_POINT ( 'NONE',  ( -18.40000000000000213, 70.35000000001261355, -190.8731074845244109 ) ) ;
#96895=CARTESIAN_POINT ( 'NONE',  ( -16.93772744219066340, 66.00645889126025168, -190.9250455125547035 ) ) ;
#97297=EDGE_LOOP ( 'NONE', ( #241873, #67906, #55219, #125444 ) ) ;
#97357=CARTESIAN_POINT ( 'NONE',  ( 18.54999999999999716, 67.25000000001251976, -182.6731074845244223 ) ) ;
#97435=AXIS2_PLACEMENT_3D ( 'NONE', #217524, #140560, #83121 ) ;
#97538=CIRCLE ( 'NONE', #110036, 0.9000000000000014655 ) ;
#97539=VECTOR ( 'NONE', #8777, 1000.000000000000000 ) ;
#97788=CARTESIAN_POINT ( 'NONE',  ( -17.11825945287482753, 66.05000000001263061, -190.7731074845244166 ) ) ;
#97811=DIRECTION ( 'NONE',  ( 0.000000000000000000, 1.000000000000000000, 6.982962677686266711E-15 ) ) ;
#98057=VECTOR ( 'NONE', #237459, 1000.000000000000000 ) ;
#98103=DIRECTION ( 'NONE',  ( -1.000000000000000000, 0.000000000000000000, -0.000000000000000000 ) ) ;
#98114=CARTESIAN_POINT ( 'NONE',  ( 12.60053434924909332, 66.61046543766585160, -187.8482981801344920 ) ) ;
#98213=CARTESIAN_POINT ( 'NONE',  ( 20.73486653747088582, 68.75000000001251976, -182.6731074845244223 ) ) ;
#98449=CARTESIAN_POINT ( 'NONE',  ( -16.90202395485879805, 66.03405545546173983, -182.6200937632638954 ) ) ;
#98497=CARTESIAN_POINT ( 'NONE',  ( -16.90137573187933739, 66.05000000001261640, -190.7346900604275675 ) ) ;
#98564=ORIENTED_EDGE ( 'NONE', *, *, #199128, .F. ) ;
#98748=ADVANCED_FACE ( 'NONE', ( #94458 ), #213127, .F. ) ;
#98844=CARTESIAN_POINT ( 'NONE',  ( -21.64999999999999858, 66.65000000001263913, -194.2731074845244166 ) ) ;
#99002=ORIENTED_EDGE ( 'NONE', *, *, #87891, .T. ) ;
#99331=B_SPLINE_CURVE_WITH_KNOTS ( 'NONE', 3,
 ( #42425, #201486, #22888, #241897, #238049, #98497, #181941, #118112, #82792, #59380 ),
 .UNSPECIFIED., .F., .F.,
 ( 4, 2, 2, 2, 4 ),
 ( 0.000000000000000000, 0.0003916577441626797819, 0.0005874866162440189410, 0.0006854010522846886019, 0.0007833154883253581544 ),
 .UNSPECIFIED. ) ;
#99337=CARTESIAN_POINT ( 'NONE',  ( -16.89268316805465986, 66.04827818677036078, -182.6673550059788909 ) ) ;
#99398=DIRECTION ( 'NONE',  ( 0.000000000000000000, 6.982962677686266711E-15, -1.000000000000000000 ) ) ;
#99589=CARTESIAN_POINT ( 'NONE',  ( -16.93658623642905070, 66.01961832835547739, -190.9112047553952038 ) ) ;
#99944=EDGE_CURVE ( 'NONE', #180338, #36544, #50644, .T. ) ;
#99947=LINE ( 'NONE', #156134, #67748 ) ;
#100104=VERTEX_POINT ( 'NONE', #257369 ) ;
#100140=CARTESIAN_POINT ( 'NONE',  ( 23.24999999999999645, 64.25000000001264766, -194.2731074845244450 ) ) ;
#100197=CYLINDRICAL_SURFACE ( 'NONE', #48296, 0.09999999999998898659 ) ;
#100653=ORIENTED_EDGE ( 'NONE', *, *, #79742, .T. ) ;
#100682=CARTESIAN_POINT ( 'NONE',  ( 15.70340296795548518, 66.64411154551001459, -187.2344645877464018 ) ) ;
#100796=AXIS2_PLACEMENT_3D ( 'NONE', #53758, #34229, #22033 ) ;
#100914=CARTESIAN_POINT ( 'NONE',  ( -16.92209698673619300, 66.05000000001255955, -182.7337430515784433 ) ) ;
#100927=ORIENTED_EDGE ( 'NONE', *, *, #10195, .F. ) ;
#101199=LINE ( 'NONE', #97357, #20809 ) ;
#101461=DIRECTION ( 'NONE',  ( 0.000000000000000000, 0.000000000000000000, 1.000000000000000000 ) ) ;
#101467=ORIENTED_EDGE ( 'NONE', *, *, #199128, .T. ) ;
#101644=CARTESIAN_POINT ( 'NONE',  ( -16.86133551771148475, 66.05000000001255955, -182.7217640499777644 ) ) ;
#101709=DIRECTION ( 'NONE',  ( 1.000000000000000000, -1.186688945009009831E-16, -8.286604613020806758E-31 ) ) ;
#101737=ORIENTED_EDGE ( 'NONE', *, *, #256767, .F. ) ;
#101782=DIRECTION ( 'NONE',  ( -1.000000000000000000, 0.000000000000000000, 0.000000000000000000 ) ) ;
#101915=ADVANCED_FACE ( 'NONE', ( #106789 ), #186351, .T. ) ;
#102001=VECTOR ( 'NONE', #209587, 1000.000000000000000 ) ;
#102221=DIRECTION ( 'NONE',  ( 0.7071067811865493491, -0.7071067811865456854, -4.937700262164518065E-15 ) ) ;
#102364=LINE ( 'NONE', #162394, #3696 ) ;
#102740=FACE_OUTER_BOUND ( 'NONE', #241740, .T. ) ;
#102934=CARTESIAN_POINT ( 'NONE',  ( -16.95709691156823240, 66.05000000001261640, -190.8630499220105321 ) ) ;
#103050=EDGE_CURVE ( 'NONE', #194584, #235005, #161392, .T. ) ;
#103070=ORIENTED_EDGE ( 'NONE', *, *, #203386, .F. ) ;
#103598=CARTESIAN_POINT ( 'NONE',  ( -16.87333278164146577, 66.11739021543380090, -183.1562752906779110 ) ) ;
#103664=CARTESIAN_POINT ( 'NONE',  ( -16.89268316805465986, 66.04827818677036078, -182.6673550059788909 ) ) ;
#103692=VERTEX_POINT ( 'NONE', #201462 ) ;
#104084=VERTEX_POINT ( 'NONE', #84401 ) ;
#104161=DIRECTION ( 'NONE',  ( -1.000000000000000000, 0.000000000000000000, 0.000000000000000000 ) ) ;
#104237=ORIENTED_EDGE ( 'NONE', *, *, #34436, .T. ) ;
#104268=CARTESIAN_POINT ( 'NONE',  ( -16.87036670365548474, 66.01058118071090064, -182.5435473672224020 ) ) ;
#104367=ORIENTED_EDGE ( 'NONE', *, *, #179802, .F. ) ;
#104788=VERTEX_POINT ( 'NONE', #223341 ) ;
#104931=CARTESIAN_POINT ( 'NONE',  ( -14.23072895065543619, 66.54401276639984530, -188.5115763176265489 ) ) ;
#105121=VECTOR ( 'NONE', #129762, 1000.000000000000000 ) ;
#105213=DIRECTION ( 'NONE',  ( 1.186688945009009831E-16, 1.000000000000000000, 6.982962677686266711E-15 ) ) ;
#105572=ORIENTED_EDGE ( 'NONE', *, *, #91490, .F. ) ;
#105615=CARTESIAN_POINT ( 'NONE',  ( -16.93353400591626112, 65.99538760383960323, -182.5904230143190148 ) ) ;
#105634=ORIENTED_EDGE ( 'NONE', *, *, #83131, .F. ) ;
#105636=EDGE_LOOP ( 'NONE', ( #139241, #201463 ) ) ;
#105870=FILL_AREA_STYLE_COLOUR ( '', #177035 ) ;
#105883=CARTESIAN_POINT ( 'NONE',  ( -17.11825945287482753, 65.95000000001262208, -190.8731074845244393 ) ) ;
#106068=CARTESIAN_POINT ( 'NONE',  ( -17.05016517655774422, 66.05000000001255955, -182.6958054805178051 ) ) ;
#106208=CARTESIAN_POINT ( 'NONE',  ( -16.86578989773641624, 66.01519019875379968, -190.9877723711466615 ) ) ;
#106237=CARTESIAN_POINT ( 'NONE',  ( -16.92563707711778775, 66.03100930561575410, -182.6423491850004552 ) ) ;
#106279=CARTESIAN_POINT ( 'NONE',  ( -16.97683809663752186, 66.15000000001261071, -190.8731074845244393 ) ) ;
#106641=DIRECTION ( 'NONE',  ( 1.186688945009010077E-16, 1.000000000000000000, 6.982962677686266711E-15 ) ) ;
#106775=CARTESIAN_POINT ( 'NONE',  ( -23.25000000000000355, 70.35000000001261355, -190.8731074845244109 ) ) ;
#106789=FACE_OUTER_BOUND ( 'NONE', #62570, .T. ) ;
#106850=ORIENTED_EDGE ( 'NONE', *, *, #34436, .F. ) ;
#106887=AXIS2_PLACEMENT_3D ( 'NONE', #106279, #144126, #202832 ) ;
#107476=CARTESIAN_POINT ( 'NONE',  ( -16.89935556175677078, 66.05000000001257376, -183.1627838474121575 ) ) ;
#107479=CARTESIAN_POINT ( 'NONE',  ( 18.39999999999999503, 64.52683809665012404, -190.8731074845244393 ) ) ;
#107561=VECTOR ( 'NONE', #47486, 1000.000000000000000 ) ;
#108204=CARTESIAN_POINT ( 'NONE',  ( 12.33938619321247998, 66.63927620602653690, -186.2091802899177253 ) ) ;
#108258=AXIS2_PLACEMENT_3D ( 'NONE', #216792, #98103, #179001 ) ;
#108355=CARTESIAN_POINT ( 'NONE',  ( -16.87333278164153683, 66.11739021543377248, -190.3899396783708085 ) ) ;
#108713=PLANE ( 'NONE',  #10171 ) ;
#108796=CARTESIAN_POINT ( 'NONE',  ( 21.13736287352038445, 67.95335762362860521, -190.8731074845244109 ) ) ;
#108824=VERTEX_POINT ( 'NONE', #153599 ) ;
#109014=CIRCLE ( 'NONE', #100796, 0.09999999999998898659 ) ;
#109072=CARTESIAN_POINT ( 'NONE',  ( -16.77828822459933633, 66.05377062495608698, -182.6857357354433589 ) ) ;
#109736=CARTESIAN_POINT ( 'NONE',  ( -16.89797118371619078, 66.02361927736880887, -190.9604008520841489 ) ) ;
#109791=LINE ( 'NONE', #207642, #174050 ) ;
#110000=DIRECTION ( 'NONE',  ( -1.000000000000000000, 1.186688945009010077E-16, 8.286604613020808509E-31 ) ) ;
#110036=AXIS2_PLACEMENT_3D ( 'NONE', #210161, #169778, #190605 ) ;
#110085=CARTESIAN_POINT ( 'NONE',  ( 23.24999999999999645, 67.17743825834614313, -182.6731074845244223 ) ) ;
#110206=SURFACE_SIDE_STYLE ('',( #128503 ) ) ;
#110258=CARTESIAN_POINT ( 'NONE',  ( -17.22767730084084192, 65.65075578754407104, -192.1655361750986515 ) ) ;
#110362=( GEOMETRIC_REPRESENTATION_CONTEXT ( 3 ) GLOBAL_UNCERTAINTY_ASSIGNED_CONTEXT ( ( #149506 ) ) GLOBAL_UNIT_ASSIGNED_CONTEXT ( ( #59879, #136871, #139420 ) ) REPRESENTATION_CONTEXT ( 'NONE', 'WORKASPACE' ) );
#110389=VERTEX_POINT ( 'NONE', #239228 ) ;
#110706=ORIENTED_EDGE ( 'NONE', *, *, #213915, .F. ) ;
#110755=CARTESIAN_POINT ( 'NONE',  ( 12.25000000000000000, 66.65000000001258229, -186.7731074845244166 ) ) ;
#110828=DIRECTION ( 'NONE',  ( 1.186688945009009831E-16, 1.000000000000000000, 6.982962677686266711E-15 ) ) ;
#110911=DIRECTION ( 'NONE',  ( -1.000000000000000000, -1.652117596168391700E-15, -1.153667551319263085E-29 ) ) ;
#111015=CIRCLE ( 'NONE', #44392, 14.30833333333333890 ) ;
#111064=EDGE_CURVE ( 'NONE', #147103, #205939, #65289, .T. ) ;
#111202=AXIS2_PLACEMENT_3D ( 'NONE', #23662, #121477, #181438 ) ;
#111319=EDGE_LOOP ( 'NONE', ( #35928, #172370, #152679, #252548, #69906 ) ) ;
#111505=( LENGTH_UNIT ( ) NAMED_UNIT ( * ) SI_UNIT ( .MILLI., .METRE. ) );
#111555=CARTESIAN_POINT ( 'NONE',  ( -16.94107738177415357, 65.98576071487597972, -190.9731074845244621 ) ) ;
#112193=AXIS2_PLACEMENT_3D ( 'NONE', #248524, #7348, #45187 ) ;
#112257=ADVANCED_FACE ( 'NONE', ( #161892 ), #120213, .F. ) ;
#112261=ORIENTED_EDGE ( 'NONE', *, *, #153022, .T. ) ;
#112520=DIRECTION ( 'NONE',  ( 1.000000000000000000, -1.186688945009010077E-16, -8.286604613020808509E-31 ) ) ;
#112682=CARTESIAN_POINT ( 'NONE',  ( -18.40000000000000213, 70.35000000001255671, -182.6731074845243938 ) ) ;
#112767=ADVANCED_FACE ( 'NONE', ( #132715 ), #195269, .F. ) ;
#112790=EDGE_CURVE ( 'NONE', #4454, #256760, #233114, .T. ) ;
#113296=VERTEX_POINT ( 'NONE', #66663 ) ;
#113420=CARTESIAN_POINT ( 'NONE',  ( -16.77683809663752257, 66.05416425680839154, -182.6870565036286393 ) ) ;
#113559=VECTOR ( 'NONE', #138488, 1000.000000000000000 ) ;
#114044=DIRECTION ( 'NONE',  ( 0.8049926720990051576, -0.5932847527679298016, -4.142885285818778274E-15 ) ) ;
#114105=CARTESIAN_POINT ( 'NONE',  ( -18.37013991200266005, 64.50025238380065673, -194.3161304950415627 ) ) ;
#114219=CARTESIAN_POINT ( 'NONE',  ( -16.78805706634180694, 66.05174750694135355, -182.6789542764925898 ) ) ;
#114234=ORIENTED_EDGE ( 'NONE', *, *, #124260, .T. ) ;
#114291=ORIENTED_EDGE ( 'NONE', *, *, #161259, .T. ) ;
#114492=EDGE_CURVE ( 'NONE', #75549, #120323, #30071, .T. ) ;
#114631=CARTESIAN_POINT ( 'NONE',  ( -16.94445028196807002, 66.00793639031481064, -182.6304376629428816 ) ) ;
#114638=CARTESIAN_POINT ( 'NONE',  ( -18.39999999999999858, 64.52132590001336609, -194.2484142681837795 ) ) ;
#114839=DIRECTION ( 'NONE',  ( 0.000000000000000000, 6.982962677686266711E-15, -1.000000000000000000 ) ) ;
#114845=EDGE_CURVE ( 'NONE', #196258, #180208, #63631, .T. ) ;
#115035=LINE ( 'NONE', #135859, #66269 ) ;
#115328=VECTOR ( 'NONE', #39405, 1000.000000000000000 ) ;
#115393=CARTESIAN_POINT ( 'NONE',  ( -16.87036670365549540, 66.01058118071094327, -191.0026676018264880 ) ) ;
#115472=ORIENTED_EDGE ( 'NONE', *, *, #187862, .T. ) ;
#115728=AXIS2_PLACEMENT_3D ( 'NONE', #127401, #105213, #6146 ) ;
#115883=EDGE_CURVE ( 'NONE', #221894, #6267, #144530, .T. ) ;
#115933=ORIENTED_EDGE ( 'NONE', *, *, #19046, .T. ) ;
#116086=CARTESIAN_POINT ( 'NONE',  ( -16.89268316805466341, 66.04827818677041762, -190.8788599630699707 ) ) ;
#116509=ADVANCED_FACE ( 'NONE', ( #141563 ), #140261, .T. ) ;
#116811=EDGE_LOOP ( 'NONE', ( #92993, #95116, #199658, #25995 ) ) ;
#117149=ORIENTED_EDGE ( 'NONE', *, *, #47550, .T. ) ;
#117343=ORIENTED_EDGE ( 'NONE', *, *, #167538, .F. ) ;
#117531=LINE ( 'NONE', #197052, #61262 ) ;
#117644=CARTESIAN_POINT ( 'NONE',  ( -16.88853107394619357, 66.04912151666556497, -182.6701711376321953 ) ) ;
#118112=CARTESIAN_POINT ( 'NONE',  ( -16.86132326855785735, 66.05000000001260219, -190.8244716998561046 ) ) ;
#118155=DIRECTION ( 'NONE',  ( 1.000000000000000000, 0.000000000000000000, 0.000000000000000000 ) ) ;
#118677=ORIENTED_EDGE ( 'NONE', *, *, #118757, .F. ) ;
#118723=DIRECTION ( 'NONE',  ( 1.000000000000000000, -7.125593699324843413E-30, 1.020425574104004196E-15 ) ) ;
#118757=EDGE_CURVE ( 'NONE', #194584, #76104, #162164, .T. ) ;
#118944=CARTESIAN_POINT ( 'NONE',  ( -16.89146115310546392, 66.04855675435608475, -182.6682850655701884 ) ) ;
#118979=CARTESIAN_POINT ( 'NONE',  ( -12.26136940704871847, 66.64859682587092493, -186.5435770476858863 ) ) ;
#119013=CARTESIAN_POINT ( 'NONE',  ( 15.15590539855246455, 66.58931770574464792, -188.0919640425762793 ) ) ;
#119057=CARTESIAN_POINT ( 'NONE',  ( -18.40000000000000213, 64.66825945288736932, -182.6731074845244507 ) ) ;
#119078=CARTESIAN_POINT ( 'NONE',  ( -16.93906926870270624, 65.98785312906605327, -190.9696551772975965 ) ) ;
#119473=CARTESIAN_POINT ( 'NONE',  ( -18.39418127959864790, 64.51609439831437953, -179.2731074845244450 ) ) ;
#119476=( BOUNDED_CURVE ( )  B_SPLINE_CURVE ( 3, ( #141568, #202826, #21636, #201538 ),
 .UNSPECIFIED., .F., .F. ) 
 B_SPLINE_CURVE_WITH_KNOTS ( ( 4, 4 ),
 ( 1.570796326794892339, 3.141592653589784678 ),
 .UNSPECIFIED. ) 
 CURVE ( )  GEOMETRIC_REPRESENTATION_ITEM ( )  RATIONAL_B_SPLINE_CURVE ( ( 1.000000000000000000, 0.8047378541243659367, 0.8047378541243659367, 1.000000000000000000 ) ) 
 REPRESENTATION_ITEM ( '' )  );
#119951=DIRECTION ( 'NONE',  ( -1.000000000000000000, -0.000000000000000000, -0.000000000000000000 ) ) ;
#120064=VECTOR ( 'NONE', #5544, 1000.000000000000000 ) ;
#120213=PLANE ( 'NONE',  #53975 ) ;
#120289=CARTESIAN_POINT ( 'NONE',  ( -14.77538296656413586, 66.56333706821347107, -185.2000707522295784 ) ) ;
#120322=ORIENTED_EDGE ( 'NONE', *, *, #54994, .T. ) ;
#120323=VERTEX_POINT ( 'NONE', #151328 ) ;
#120371=DIRECTION ( 'NONE',  ( -1.000000000000000000, 0.000000000000000000, 0.000000000000000000 ) ) ;
#120382=CARTESIAN_POINT ( 'NONE',  ( -18.40000000000000213, 64.51332499825484490, -179.2731074845244450 ) ) ;
#120461=CARTESIAN_POINT ( 'NONE',  ( -16.98495255085918032, 65.99443563401784729, -190.8884902783039195 ) ) ;
#120713=CARTESIAN_POINT ( 'NONE',  ( -13.22483237240080101, 66.56332574816974557, -188.3462455535252218 ) ) ;
#120727=CARTESIAN_POINT ( 'NONE',  ( -17.22767730082141213, 65.65075578754381525, -181.3806787939495848 ) ) ;
#120915=DIRECTION ( 'NONE',  ( -0.7071067811865463515, 0.7071067811865487940, 4.178957128135655137E-15 ) ) ;
#121117=VECTOR ( 'NONE', #220989, 1000.000000000000000 ) ;
#121396=( BOUNDED_SURFACE ( )  B_SPLINE_SURFACE ( 3, 2, ( 
 ( #129201, #165774, #47067 ),
 ( #186615, #7973, #127918 ),
 ( #90051, #207462, #108355 ),
 ( #50906, #167071, #187896 ),
 ( #67931, #249159, #208747 ),
 ( #9239, #30115, #150065 ),
 ( #130470, #75663, #74395 ),
 ( #177346, #93913, #134307 ),
 ( #152643, #232164, #53508 ),
 ( #16967, #235987, #35268 ) ),
 .UNSPECIFIED., .F., .F., .T. ) 
 B_SPLINE_SURFACE_WITH_KNOTS ( ( 4, 2, 2, 2, 4 ),
 ( 3, 3 ),
 ( 0.002161241639767812889, 0.002579950749617465015, 0.002789305304542291294, 0.002893982582004704217, 0.002998659859467117141 ),
 ( 0.000000000000000000, 1.000000000000000000 ),
 .UNSPECIFIED. ) 
 GEOMETRIC_REPRESENTATION_ITEM ( )  RATIONAL_B_SPLINE_SURFACE ( (
 ( 1.000000000000000000, 0.7071067811864985009, 1.000000000000000000),
 ( 1.000000000000000000, 0.7632447400666618753, 1.000000000000000000),
 ( 1.000000000000000000, 0.8158073005106054598, 1.000000000000000000),
 ( 1.000000000000000000, 0.8906973462397409502, 1.000000000000000000),
 ( 1.000000000000000000, 0.9149408947796440206, 1.000000000000000000),
 ( 1.000000000000000000, 0.9493368785277611632, 1.000000000000000000),
 ( 1.000000000000000000, 0.9605194247158402865, 1.000000000000000000),
 ( 1.000000000000000000, 0.9803630264779391590, 1.000000000000000000),
 ( 1.000000000000000000, 0.9900844824272457823, 1.000000000000000000),
 ( 1.000000000000000000, 0.9894588281429252952, 1.000000000000000000) ) ) 
 REPRESENTATION_ITEM ( '' )  SURFACE ( )  );
#121477=DIRECTION ( 'NONE',  ( -1.073024830501117725E-15, 6.982962677686266711E-15, -1.000000000000000000 ) ) ;
#121515=CARTESIAN_POINT ( 'NONE',  ( -16.77683809663752257, 66.05416425680844839, -190.8591584654202222 ) ) ;
#121570=CARTESIAN_POINT ( 'NONE',  ( -13.77083647240105257, 66.54258906972242471, -185.0231915757781564 ) ) ;
#121622=B_SPLINE_CURVE_WITH_KNOTS ( 'NONE', 3,
 ( #207264, #3910, #221649, #143415, #202113, #67732, #182565, #44330, #82130, #104268 ),
 .UNSPECIFIED., .F., .F.,
 ( 4, 3, 3, 4 ),
 ( 7.632826238681267430E-06, 4.756916949875584252E-05, 9.484459048148792613E-05, 0.0001435500935099677739 ),
 .UNSPECIFIED. ) ;
#121632=DIRECTION ( 'NONE',  ( -0.000000000000000000, -6.982962677686266711E-15, 1.000000000000000000 ) ) ;
#121894=CARTESIAN_POINT ( 'NONE',  ( -20.65000000000000568, 68.75000000001256240, -182.6731074845244223 ) ) ;
#121970=DIRECTION ( 'NONE',  ( 1.186688945009010077E-16, 1.000000000000000000, 6.982962677686266711E-15 ) ) ;
#122085=B_SPLINE_CURVE_WITH_KNOTS ( 'NONE', 3,
 ( #88192, #52940, #231600, #206890, #150768, #229031, #50353, #47791, #209449, #226424, #191207, #12562, #166508 ),
 .UNSPECIFIED., .F., .F.,
 ( 4, 3, 3, 3, 4 ),
 ( 1.075528555105620399E-16, 1.946463881814325270E-05, 3.922356109943460204E-05, 4.215060953239334383E-05, 4.415117091092807429E-05 ),
 .UNSPECIFIED. ) ;
#122100=CARTESIAN_POINT ( 'NONE',  ( 18.39999999999999503, 64.25000000001261924, -190.8731074845244393 ) ) ;
#122295=ORIENTED_EDGE ( 'NONE', *, *, #206763, .T. ) ;
#122316=ORIENTED_EDGE ( 'NONE', *, *, #179802, .T. ) ;
#122536=CARTESIAN_POINT ( 'NONE',  ( -17.04295772865477687, 65.97510057475108169, -190.8731074845244109 ) ) ;
#122613=DIRECTION ( 'NONE',  ( 1.000000000000000000, 0.000000000000000000, 0.000000000000000000 ) ) ;
#122863=MECHANICAL_DESIGN_GEOMETRIC_PRESENTATION_REPRESENTATION('',(#218487),#110362);
#123193=CARTESIAN_POINT ( 'NONE',  ( -16.80070461187868247, 66.05000000001255955, -182.6700713136814045 ) ) ;
#123202=CARTESIAN_POINT ( 'NONE',  ( -16.92973740335360588, 66.00749618554401366, -182.6170484493211461 ) ) ;
#123210=CARTESIAN_POINT ( 'NONE',  ( -18.39999999999999858, 64.52683809665015247, -194.1971614177164724 ) ) ;
#123397=LINE ( 'NONE', #183376, #213476 ) ;
#123499=PRODUCT_DEFINITION_CONTEXT ( 'detailed design', #125842, 'design' ) ;
#123737=ORIENTED_EDGE ( 'NONE', *, *, #210026, .F. ) ;
#123922=CARTESIAN_POINT ( 'NONE',  ( 15.74999999999999289, 66.65000000001258229, -186.6573643172504831 ) ) ;
#124066=ORIENTED_EDGE ( 'NONE', *, *, #19046, .F. ) ;
#124260=EDGE_CURVE ( 'NONE', #79239, #127125, #73906, .T. ) ;
#124360=CARTESIAN_POINT ( 'NONE',  ( -16.94107738177414291, 65.98576071487592287, -182.5731074845244279 ) ) ;
#124458=ADVANCED_FACE ( 'NONE', ( #718 ), #204750, .T. ) ;
#124565=CARTESIAN_POINT ( 'NONE',  ( -17.73285935862697826, 65.14201819622552136, -180.2645456747497121 ) ) ;
#124739=CYLINDRICAL_SURFACE ( 'NONE', #112193, 1.749999999999999778 ) ;
#124749=EDGE_CURVE ( 'NONE', #74091, #45497, #190977, .T. ) ;
#125214=ORIENTED_EDGE ( 'NONE', *, *, #258026, .F. ) ;
#125225=EDGE_LOOP ( 'NONE', ( #101467, #76765, #243513, #81789 ) ) ;
#125283=PLANE ( 'NONE',  #215952 ) ;
#125366=AXIS2_PLACEMENT_3D ( 'NONE', #38521, #60625, #1933 ) ;
#125444=ORIENTED_EDGE ( 'NONE', *, *, #232392, .T. ) ;
#125588=CARTESIAN_POINT ( 'NONE',  ( -23.25000000000000355, 70.35000000001264198, -194.2731074845243882 ) ) ;
#125626=VERTEX_POINT ( 'NONE', #116086 ) ;
#125734=ORIENTED_EDGE ( 'NONE', *, *, #62454, .F. ) ;
#125735=CARTESIAN_POINT ( 'NONE',  ( 18.39999999999997371, 64.52683809665003878, -179.2731074845244450 ) ) ;
#125811=CARTESIAN_POINT ( 'NONE',  ( -13.54795643572458985, 66.54933111084503139, -188.4675609943170400 ) ) ;
#125842=APPLICATION_CONTEXT ( 'automotive_design' ) ;
#126471=CARTESIAN_POINT ( 'NONE',  ( 12.26145404764308822, 66.64858632091117840, -186.5427639169754173 ) ) ;
#126600=ORIENTED_EDGE ( 'NONE', *, *, #64251, .T. ) ;
#126627=VECTOR ( 'NONE', #97811, 1000.000000000000000 ) ;
#126949=DIRECTION ( 'NONE',  ( 0.000000000000000000, 6.982962677686266711E-15, -1.000000000000000000 ) ) ;
#126994=CARTESIAN_POINT ( 'NONE',  ( -12.25000000000000178, 66.15000000001258229, -186.7731074845244166 ) ) ;
#127125=VERTEX_POINT ( 'NONE', #26999 ) ;
#127262=VECTOR ( 'NONE', #43557, 1000.000000000000000 ) ;
#127401=CARTESIAN_POINT ( 'NONE',  ( 13.99999999999999822, 66.15000000001258229, -186.7731074845244450 ) ) ;
#127468=DIRECTION ( 'NONE',  ( 0.000000000000000000, -6.982962677686266711E-15, 1.000000000000000000 ) ) ;
#127520=CARTESIAN_POINT ( 'NONE',  ( -14.00000000000000178, 66.15000000001258229, -186.7731074845244166 ) ) ;
#127654=DIRECTION ( 'NONE',  ( -1.000000000000000000, 0.000000000000000000, 0.000000000000000000 ) ) ;
#127918=CARTESIAN_POINT ( 'NONE',  ( -16.87683809663752754, 66.13411015068207632, -190.2556806774549898 ) ) ;
#128223=ADVANCED_FACE ( 'NONE', ( #85658 ), #183525, .T. ) ;
#128361=CARTESIAN_POINT ( 'NONE',  ( 20.05000000000002913, 68.75000000001251976, -182.6731074845244223 ) ) ;
#128503=SURFACE_STYLE_FILL_AREA ( #11125 ) ;
#128752=CARTESIAN_POINT ( 'NONE',  ( -16.87683809663752399, 66.15000000001261071, -190.8731074845244393 ) ) ;
#129145=CARTESIAN_POINT ( 'NONE',  ( 18.39999999999998082, 64.52683809665015247, -194.2731074845244450 ) ) ;
#129201=CARTESIAN_POINT ( 'NONE',  ( -16.97683809663752186, 66.05000000001261640, -190.1207434663279514 ) ) ;
#129318=CARTESIAN_POINT ( 'NONE',  ( -16.92778301347241054, 65.99905508317772274, -190.9516255924938264 ) ) ;
#129357=DIRECTION ( 'NONE',  ( 1.073024830501117725E-15, -6.982962677686266711E-15, 1.000000000000000000 ) ) ;
#129599=EDGE_CURVE ( 'NONE', #199626, #73216, #119476, .T. ) ;
#129672=CARTESIAN_POINT ( 'NONE',  ( -12.25000000000000178, 66.65000000001258229, -186.7731074845244166 ) ) ;
#129762=DIRECTION ( 'NONE',  ( -0.000000000000000000, -6.982962677686266711E-15, 1.000000000000000000 ) ) ;
#129775=( NAMED_UNIT ( * ) SI_UNIT ( $, .STERADIAN. ) SOLID_ANGLE_UNIT ( ) );
#130001=LINE ( 'NONE', #128752, #206609 ) ;
#130180=DIRECTION ( 'NONE',  ( 0.000000000000000000, -6.982962677686266711E-15, 1.000000000000000000 ) ) ;
#130417=CARTESIAN_POINT ( 'NONE',  ( 16.87683809663750267, 66.05000000001261640, -190.8731074845244393 ) ) ;
#130470=CARTESIAN_POINT ( 'NONE',  ( -16.87401514999222840, 66.05000000001261640, -190.8031254770564829 ) ) ;
#130931=CARTESIAN_POINT ( 'NONE',  ( -16.86337532320261801, 66.02003279578825357, -190.9720319535072406 ) ) ;
#130938=ORIENTED_EDGE ( 'NONE', *, *, #245413, .F. ) ;
#130997=VERTEX_POINT ( 'NONE', #257341 ) ;
#131108=CARTESIAN_POINT ( 'NONE',  ( -17.29838795460011625, 65.62845014205002769, -192.1278487671402786 ) ) ;
#131624=CARTESIAN_POINT ( 'NONE',  ( 21.72449340488910607, 65.71604372252143378, -182.6731074845244223 ) ) ;
#131698=CARTESIAN_POINT ( 'NONE',  ( -16.83794479845801462, 66.07364258066102991, -182.8266627803020867 ) ) ;
#131991=VERTEX_POINT ( 'NONE', #143268 ) ;
#132143=CARTESIAN_POINT ( 'NONE',  ( -16.87383368123029825, 66.05000000001261640, -190.8731074845244393 ) ) ;
#132310=ORIENTED_EDGE ( 'NONE', *, *, #156087, .F. ) ;
#132403=CARTESIAN_POINT ( 'NONE',  ( -17.78241384945274461, 65.14442424721148939, -193.2740698120442744 ) ) ;
#132494=ORIENTED_EDGE ( 'NONE', *, *, #214438, .F. ) ;
#132715=FACE_OUTER_BOUND ( 'NONE', #59425, .T. ) ;
#132894=DIRECTION ( 'NONE',  ( 0.000000000000000000, 1.000000000000000000, 0.000000000000000000 ) ) ;
#132934=CARTESIAN_POINT ( 'NONE',  ( -18.39999999999999858, 64.52683809665015247, -194.1971614177164724 ) ) ;
#132993=ORIENTED_EDGE ( 'NONE', *, *, #74093, .F. ) ;
#132998=CARTESIAN_POINT ( 'NONE',  ( -16.80100914604134843, 66.05685090590898767, -182.7060633572368147 ) ) ;
#133076=FACE_OUTER_BOUND ( 'NONE', #88232, .T. ) ;
#133174=CARTESIAN_POINT ( 'NONE',  ( -16.91256925476572093, 66.01426884188440170, -190.9907499735296881 ) ) ;
#133373=CARTESIAN_POINT ( 'NONE',  ( 20.73486653747088226, 68.75000000001257661, -190.8731074845244109 ) ) ;
#133405=AXIS2_PLACEMENT_3D ( 'NONE', #133671, #33331, #248488 ) ;
#133657=LINE ( 'NONE', #37146, #166233 ) ;
#133671=CARTESIAN_POINT ( 'NONE',  ( 20.99999999999999645, 66.25000000001264766, -194.2731074845244166 ) ) ;
#133966=LINE ( 'NONE', #15338, #32174 ) ;
#134091=ORIENTED_EDGE ( 'NONE', *, *, #232392, .F. ) ;
#134246=CARTESIAN_POINT ( 'NONE',  ( -16.87372397896795562, 66.11940046337079480, -183.1723829744886700 ) ) ;
#134282=ORIENTED_EDGE ( 'NONE', *, *, #112790, .T. ) ;
#134307=CARTESIAN_POINT ( 'NONE',  ( -16.80621392010917958, 66.05779742250486208, -190.8335155191072374 ) ) ;
#135160=DIRECTION ( 'NONE',  ( 0.000000000000000000, 0.000000000000000000, 1.000000000000000000 ) ) ;
#135296=CARTESIAN_POINT ( 'NONE',  ( -18.34374000495060386, 64.52683809665015247, -194.2731074845244450 ) ) ;
#135464=VERTEX_POINT ( 'NONE', #167258 ) ;
#135759=CIRCLE ( 'NONE', #56464, 0.9000000000000014655 ) ;
#135859=CARTESIAN_POINT ( 'NONE',  ( -21.64999999999999858, 66.65000000001261071, -190.8731074845244393 ) ) ;
#135974=CARTESIAN_POINT ( 'NONE',  ( 14.56326696814971555, 66.55335100938374637, -188.4339441886012594 ) ) ;
#136076=ORIENTED_EDGE ( 'NONE', *, *, #74804, .T. ) ;
#136108=LINE ( 'NONE', #17472, #169486 ) ;
#136172=CARTESIAN_POINT ( 'NONE',  ( -23.25000000000000355, 64.25000000001256240, -182.6731074845244507 ) ) ;
#136194=ADVANCED_FACE ( 'NONE', ( #161672 ), #31167, .T. ) ;
#136592=CARTESIAN_POINT ( 'NONE',  ( -18.40000000000000213, 64.66825945288744037, -190.8731074845244393 ) ) ;
#136630=DIRECTION ( 'NONE',  ( 1.000000000000000000, 0.000000000000000000, 0.000000000000000000 ) ) ;
#136631=DIRECTION ( 'NONE',  ( -1.000000000000000000, 7.492892343619937423E-30, -1.073024830501117725E-15 ) ) ;
#136843=CARTESIAN_POINT ( 'NONE',  ( 20.27550659511089037, 66.78395627750370522, -182.6731074845244223 ) ) ;
#136854=CARTESIAN_POINT ( 'NONE',  ( 23.04999999999999716, 67.17743825834614313, -182.6731074845244223 ) ) ;
#136871=( NAMED_UNIT ( * ) PLANE_ANGLE_UNIT ( ) SI_UNIT ( $, .RADIAN. ) );
#136918=PLANE ( 'NONE',  #156175 ) ;
#137104=EDGE_CURVE ( 'NONE', #169837, #207406, #207562, .T. ) ;
#137182=VECTOR ( 'NONE', #77905, 1000.000000000000000 ) ;
#137261=EDGE_LOOP ( 'NONE', ( #209216, #210425, #17076, #198004 ) ) ;
#137268=CARTESIAN_POINT ( 'NONE',  ( 13.22261339317535267, 66.56344716000816675, -188.3451520117641564 ) ) ;
#137358=CARTESIAN_POINT ( 'NONE',  ( 18.39999999999999503, 64.25000000001261924, -190.8731074845244393 ) ) ;
#137599=CARTESIAN_POINT ( 'NONE',  ( -16.91256925476571382, 66.01426884188435906, -182.5554649955192019 ) ) ;
#137607=CYLINDRICAL_SURFACE ( 'NONE', #191757, 1.500000000000001332 ) ;
#137915=ORIENTED_EDGE ( 'NONE', *, *, #210, .F. ) ;
#138324=EDGE_CURVE ( 'NONE', #42728, #154893, #188119, .T. ) ;
#138472=LINE ( 'NONE', #133373, #69467 ) ;
#138488=DIRECTION ( 'NONE',  ( 0.000000000000000000, -6.982962677686266711E-15, 1.000000000000000000 ) ) ;
#138531=CARTESIAN_POINT ( 'NONE',  ( 13.88302573338719981, 66.54258905524520173, -188.5230235107344470 ) ) ;
#138732=CARTESIAN_POINT ( 'NONE',  ( -17.78043020864321022, 65.14640788800683424, -180.3600583188042208 ) ) ;
#138787=ADVANCED_FACE ( 'NONE', ( #44042 ), #218810, .F. ) ;
#138855=DIRECTION ( 'NONE',  ( -0.000000000000000000, -6.982962677686266711E-15, 1.000000000000000000 ) ) ;
#139241=ORIENTED_EDGE ( 'NONE', *, *, #91490, .T. ) ;
#139247=ORIENTED_EDGE ( 'NONE', *, *, #74093, .T. ) ;
#139268=DIRECTION ( 'NONE',  ( -1.000000000000000000, -1.652117596168391700E-15, -1.153667551319263085E-29 ) ) ;
#139420=( NAMED_UNIT ( * ) SI_UNIT ( $, .STERADIAN. ) SOLID_ANGLE_UNIT ( ) );
#139593=CARTESIAN_POINT ( 'NONE',  ( 15.69410316191959254, 66.64325398293429714, -186.3197477631601942 ) ) ;
#139644=DIRECTION ( 'NONE',  ( -1.000000000000000000, 0.000000000000000000, -0.000000000000000000 ) ) ;
#139893=CARTESIAN_POINT ( 'NONE',  ( -16.93909480342659890, 66.00692163521105726, -190.9227604678521004 ) ) ;
#139914=ORIENTED_EDGE ( 'NONE', *, *, #79263, .F. ) ;
#140187=EDGE_LOOP ( 'NONE', ( #71663, #32444, #156995, #13638 ) ) ;
#140239=CARTESIAN_POINT ( 'NONE',  ( -16.91256925476569606, 66.01426884188437327, -182.5554649955192019 ) ) ;
#140261=PLANE ( 'NONE',  #176444 ) ;
#140560=DIRECTION ( 'NONE',  ( 1.186688945009010077E-16, 1.000000000000000000, 6.982962677686266711E-15 ) ) ;
#140648=EDGE_LOOP ( 'NONE', ( #185109, #6836, #98564, #114291 ) ) ;
#140912=CARTESIAN_POINT ( 'NONE',  ( 13.88638282980484284, 66.54257354752368769, -185.0230656161244553 ) ) ;
#141031=CARTESIAN_POINT ( 'NONE',  ( 20.73486653747088582, 68.75000000001259082, -194.2731074845244166 ) ) ;
#141141=CARTESIAN_POINT ( 'NONE',  ( 14.87567385445977308, 66.56923500459026855, -188.2925700897740455 ) ) ;
#141442=DIRECTION ( 'NONE',  ( 0.000000000000000000, -6.982962677686266711E-15, 1.000000000000000000 ) ) ;
#141563=FACE_OUTER_BOUND ( 'NONE', #32262, .T. ) ;
#141568=CARTESIAN_POINT ( 'NONE',  ( -18.40000000000000213, 64.66825945288744037, -190.8731074845244393 ) ) ;
#141750=ORIENTED_EDGE ( 'NONE', *, *, #53591, .T. ) ;
#142030=CARTESIAN_POINT ( 'NONE',  ( 20.99999999999999645, 66.25000000001264766, -194.2731074845244166 ) ) ;
#142149=CYLINDRICAL_SURFACE ( 'NONE', #51684, 1.749999999999998002 ) ;
#142183=CARTESIAN_POINT ( 'NONE',  ( 13.22461703343584816, 66.56333706821347107, -185.2000707522295215 ) ) ;
#142368=DIRECTION ( 'NONE',  ( -1.000000000000000000, -0.000000000000000000, -0.000000000000000000 ) ) ;
#142556=LINE ( 'NONE', #61749, #3391 ) ;
#142570=EDGE_LOOP ( 'NONE', ( #33388, #154403, #46241, #65797, #3569, #170094, #53463, #65434, #243353, #241995, #30620, #23476 ) ) ;
#142665=EDGE_LOOP ( 'NONE', ( #195024, #6878, #46586, #12556 ) ) ;
#142715=VERTEX_POINT ( 'NONE', #191653 ) ;
#142718=FACE_OUTER_BOUND ( 'NONE', #22509, .T. ) ;
#142733=CARTESIAN_POINT ( 'NONE',  ( -16.79270642812263503, 66.05375578307393880, -182.6841742059602041 ) ) ;
#142788=CARTESIAN_POINT ( 'NONE',  ( -15.75000000000000355, 66.65000000001258229, -187.0015881126992952 ) ) ;
#142801=CARTESIAN_POINT ( 'NONE',  ( -18.44085059012132177, 64.48598750652871558, -179.2828021654028987 ) ) ;
#143198=AXIS2_PLACEMENT_3D ( 'NONE', #96545, #118723, #29 ) ;
#143268=CARTESIAN_POINT ( 'NONE',  ( -16.81744102076748959, 66.05000000001255955, -182.6731074845244223 ) ) ;
#143415=CARTESIAN_POINT ( 'NONE',  ( -16.87304349924914604, 66.03825492205537273, -182.6340408094791883 ) ) ;
#143433=DIRECTION ( 'NONE',  ( 1.186688945009010077E-16, 1.000000000000000000, 6.982962677686266711E-15 ) ) ;
#143444=ORIENTED_EDGE ( 'NONE', *, *, #214522, .F. ) ;
#143655=CARTESIAN_POINT ( 'NONE',  ( -14.11361717019514472, 66.54257354752367348, -185.0230656161243701 ) ) ;
#143733=SURFACE_STYLE_USAGE ( .BOTH. , #42098 ) ;
#143933=FACE_OUTER_BOUND ( 'NONE', #111319, .T. ) ;
#143955=ORIENTED_EDGE ( 'NONE', *, *, #161545, .F. ) ;
#143969=FACE_OUTER_BOUND ( 'NONE', #61304, .T. ) ;
#144083=PRODUCT_DEFINITION ( 'UNKNOWN', '', #65503, #123499 ) ;
#144126=DIRECTION ( 'NONE',  ( 0.000000000000000000, -6.982962677686266711E-15, 1.000000000000000000 ) ) ;
#144243=CARTESIAN_POINT ( 'NONE',  ( -20.65000000000000568, 70.35000000001264198, -194.2731074845243882 ) ) ;
#144286=CARTESIAN_POINT ( 'NONE',  ( 23.24999999999999645, 64.25000000001256240, -182.6731074845244507 ) ) ;
#144530=B_SPLINE_CURVE_WITH_KNOTS ( 'NONE', 3,
 ( #82180, #123922, #60072, #139593, #199620, #20989, #180041, #80911, #63937, #44383, #240012, #61364, #202164, #140912, #161776, #241305, #62662, #142183, #43093, #144733, #169495, #224285, #225544, #45658, #189018, #108204, #187750, #126471, #67781, #110755 ),
 .UNSPECIFIED., .F., .F.,
 ( 4, 2, 2, 2, 2, 2, 2, 2, 2, 2, 2, 2, 2, 2, 4 ),
 ( 0.000000000000000000, 0.0003422764154113056966, 0.0006845528308226113932, 0.001026829246233917090, 0.001369105661645222786, 0.002053658492467898798, 0.002738211323290575677, 0.003080487738701916719, 0.003422764154113257327, 0.003765040569524598368, 0.004107316984935938976, 0.004449593400347280452, 0.004791869815758621060, 0.005134146231169961667, 0.005476422646581303143 ),
 .UNSPECIFIED. ) ;
#144574=CARTESIAN_POINT ( 'NONE',  ( 20.73486653747088937, 68.25000000001257661, -190.8731074845244109 ) ) ;
#144733=CARTESIAN_POINT ( 'NONE',  ( 12.93279065517213766, 66.58230930894947619, -185.3815067877598040 ) ) ;
#144843=CARTESIAN_POINT ( 'NONE',  ( -16.87036670365549895, 66.01058118071095748, -191.0026676018264880 ) ) ;
#145263=DIRECTION ( 'NONE',  ( 0.000000000000000000, -1.000000000000000000, -7.813886390323680189E-15 ) ) ;
#145304=CARTESIAN_POINT ( 'NONE',  ( -16.88705144915432044, 66.05000000001257376, -182.9540860792355375 ) ) ;
#145313=EDGE_CURVE ( 'NONE', #195865, #24375, #91078, .T. ) ;
#145375=CARTESIAN_POINT ( 'NONE',  ( -14.45443560709638042, 66.54940788787891393, -188.4669191657160923 ) ) ;
#145486=SURFACE_STYLE_USAGE ( .BOTH. , #110206 ) ;
#145654=APPLICATION_CONTEXT ( 'automotive_design' ) ;
#145660=EDGE_CURVE ( 'NONE', #125626, #42728, #230072, .T. ) ;
#145774=EDGE_CURVE ( 'NONE', #75549, #75787, #197428, .T. ) ;
#145872=ORIENTED_EDGE ( 'NONE', *, *, #115883, .F. ) ;
#146120=CARTESIAN_POINT ( 'NONE',  ( 22.88900146558018989, 67.29609520889972885, -182.6731074845244223 ) ) ;
#146141=DIRECTION ( 'NONE',  ( -1.073024830501117725E-15, -6.982962677686266711E-15, 1.000000000000000000 ) ) ;
#146370=ORIENTED_EDGE ( 'NONE', *, *, #188048, .F. ) ;
#146540=CARTESIAN_POINT ( 'NONE',  ( -16.87683809663752399, 52.34166666667924517, -186.7731074845245303 ) ) ;
#146643=CARTESIAN_POINT ( 'NONE',  ( -14.56556274378148430, 66.55344247694006299, -188.4331655301785986 ) ) ;
#146910=EDGE_CURVE ( 'NONE', #113296, #100104, #242046, .T. ) ;
#147103=VERTEX_POINT ( 'NONE', #11016 ) ;
#147209=CARTESIAN_POINT ( 'NONE',  ( 23.04999999999999716, 67.17743825834622839, -194.2731074845244166 ) ) ;
#147282=VERTEX_POINT ( 'NONE', #98213 ) ;
#147421=CYLINDRICAL_SURFACE ( 'NONE', #209697, 0.1000000000000038219 ) ;
#147493=FACE_OUTER_BOUND ( 'NONE', #185965, .T. ) ;
#147903=CARTESIAN_POINT ( 'NONE',  ( -16.80621392010912629, 66.05779742250483366, -182.7126994499415957 ) ) ;
#148203=EDGE_CURVE ( 'NONE', #188385, #125626, #166773, .T. ) ;
#148281=CARTESIAN_POINT ( 'NONE',  ( -17.11825945287481332, 66.05000000001255955, -182.7731074845244450 ) ) ;
#148285=ORIENTED_EDGE ( 'NONE', *, *, #2026, .F. ) ;
#148848=CARTESIAN_POINT ( 'NONE',  ( -20.65000000000000568, 70.35000000001255671, -182.6731074845243938 ) ) ;
#148871=CARTESIAN_POINT ( 'NONE',  ( -18.40000000000000213, 64.25000000001261924, -190.8731074845244393 ) ) ;
#149195=LINE ( 'NONE', #90467, #177811 ) ;
#149506=UNCERTAINTY_MEASURE_WITH_UNIT (LENGTH_MEASURE( 1.000000000000000082E-05 ), #59879, 'distance_accuracy_value', 'NONE');
#149566=EDGE_CURVE ( 'NONE', #113296, #104084, #231413, .T. ) ;
#149627=CARTESIAN_POINT ( 'NONE',  ( -18.34374000495059676, 64.52683809665003878, -179.2731074845244450 ) ) ;
#149631=CARTESIAN_POINT ( 'NONE',  ( 18.39999999999999503, 70.35000000001255671, -182.6731074845243938 ) ) ;
#149651=LINE ( 'NONE', #195201, #53593 ) ;
#149841=VECTOR ( 'NONE', #142368, 1000.000000000000000 ) ;
#149975=CARTESIAN_POINT ( 'NONE',  ( 12.25000000000000000, 66.15000000001258229, -186.7731074845244450 ) ) ;
#150011=CARTESIAN_POINT ( 'NONE',  ( 17.23472005113828232, 65.69211804551183320, -192.0696843445931563 ) ) ;
#150065=CARTESIAN_POINT ( 'NONE',  ( -16.83233564386403813, 66.06977820342787311, -190.7476281480005014 ) ) ;
#150181=CARTESIAN_POINT ( 'NONE',  ( -16.89318236219977010, 66.04846474213746887, -190.8782371166302880 ) ) ;
#150253=CARTESIAN_POINT ( 'NONE',  ( -17.04761207306817283, 65.97354912661477044, -182.6731074845243938 ) ) ;
#150768=CARTESIAN_POINT ( 'NONE',  ( -16.79184697841823848, 66.05123833835421010, -190.8689652139219106 ) ) ;
#150981=EDGE_LOOP ( 'NONE', ( #2344, #23076, #30006, #229621, #55914, #74854 ) ) ;
#151278=CARTESIAN_POINT ( 'NONE',  ( -16.87683809663752044, 66.13508655273233217, -183.2988259332204564 ) ) ;
#151328=CARTESIAN_POINT ( 'NONE',  ( -18.40000000000000213, 64.52683809665003878, -179.3490535513324176 ) ) ;
#151398=AXIS2_PLACEMENT_3D ( 'NONE', #98844, #139268, #179719 ) ;
#151473=CARTESIAN_POINT ( 'NONE',  ( -16.90202395485728459, 66.03405545546350197, -190.9261212057837440 ) ) ;
#151588=AXIS2_PLACEMENT_3D ( 'NONE', #18061, #96302, #132894 ) ;
#151694=CARTESIAN_POINT ( 'NONE',  ( 18.39999999999999503, 70.35000000001255671, -182.6731074845243938 ) ) ;
#152098=DIRECTION ( 'NONE',  ( -1.000000000000000000, 0.000000000000000000, 0.000000000000000000 ) ) ;
#152251=CARTESIAN_POINT ( 'NONE',  ( -16.79139129368504157, 66.05505583755092402, -190.8528628516986316 ) ) ;
#152556=EDGE_CURVE ( 'NONE', #131991, #135464, #245885, .T. ) ;
#152607=DIRECTION ( 'NONE',  ( -1.073024830501117725E-15, 6.982962677686266711E-15, -1.000000000000000000 ) ) ;
#152643=CARTESIAN_POINT ( 'NONE',  ( -16.80891096016297226, 66.05000000001261640, -190.8907702917946096 ) ) ;
#152679=ORIENTED_EDGE ( 'NONE', *, *, #176150, .F. ) ;
#152797=ADVANCED_FACE ( 'NONE', ( #199193 ), #35022, .F. ) ;
#152825=DIRECTION ( 'NONE',  ( -0.000000000000000000, -6.982962677686266711E-15, 1.000000000000000000 ) ) ;
#152853=VECTOR ( 'NONE', #139644, 1000.000000000000000 ) ;
#152888=EDGE_LOOP ( 'NONE', ( #103070, #60924, #163195, #56061, #43366, #233447, #256330, #5537, #26931, #195308, #11755, #27762, #137915, #203129 ) ) ;
#152940=( BOUNDED_CURVE ( )  B_SPLINE_CURVE ( 3, ( #256457, #214827, #19202, #156173 ),
 .UNSPECIFIED., .F., .F. ) 
 B_SPLINE_CURVE_WITH_KNOTS ( ( 4, 4 ),
 ( 0.5235987755982449698, 1.570796326794896558 ),
 .UNSPECIFIED. ) 
 CURVE ( )  GEOMETRIC_REPRESENTATION_ITEM ( )  RATIONAL_B_SPLINE_CURVE ( ( 1.000000000000000000, 0.9106836025229499976, 0.9106836025229499976, 1.000000000000000000 ) ) 
 REPRESENTATION_ITEM ( '' )  );
#152960=CARTESIAN_POINT ( 'NONE',  ( -16.77683809663752257, 52.34166666667924517, -186.7731074845245303 ) ) ;
#153022=EDGE_CURVE ( 'NONE', #178117, #193731, #122085, .T. ) ;
#153151=ORIENTED_EDGE ( 'NONE', *, *, #72904, .F. ) ;
#153513=CARTESIAN_POINT ( 'NONE',  ( 0.000000000000000000, 0.000000000000000000, 0.000000000000000000 ) ) ;
#153599=CARTESIAN_POINT ( 'NONE',  ( 16.87683809663750267, 66.05000000001261640, -190.8731074845244393 ) ) ;
#153602=DIRECTION ( 'NONE',  ( -1.020425574104004196E-15, -6.982962677686266711E-15, 1.000000000000000000 ) ) ;
#153700=EDGE_CURVE ( 'NONE', #100104, #36544, #121622, .T. ) ;
#153775=DIRECTION ( 'NONE',  ( 1.000000000000000000, 0.000000000000000000, 0.000000000000000000 ) ) ;
#153929=EDGE_CURVE ( 'NONE', #76475, #160738, #258007, .T. ) ;
#153986=AXIS2_PLACEMENT_3D ( 'NONE', #136854, #152607, #194297 ) ;
#154210=DIRECTION ( 'NONE',  ( -0.000000000000000000, -6.982962677686266711E-15, 1.000000000000000000 ) ) ;
#154403=ORIENTED_EDGE ( 'NONE', *, *, #214169, .F. ) ;
#154481=DIRECTION ( 'NONE',  ( -1.020425574104004196E-15, 6.982962677686266711E-15, -1.000000000000000000 ) ) ;
#154551=DIRECTION ( 'NONE',  ( -0.7071067811865456854, -0.7071067811865493491, -4.937700262164544098E-15 ) ) ;
#154606=CARTESIAN_POINT ( 'NONE',  ( -18.39999999999999858, 64.52683809665015247, -194.1971614177164724 ) ) ;
#154762=CARTESIAN_POINT ( 'NONE',  ( -18.38204789744325396, 64.52049896284744079, -179.2731074845244450 ) ) ;
#154819=CARTESIAN_POINT ( 'NONE',  ( -16.81930730667007623, 66.06300193113855812, -190.7963397539862740 ) ) ;
#154859=CARTESIAN_POINT ( 'NONE',  ( -16.27683809663751191, 66.65000000001263913, -194.2731074845244450 ) ) ;
#154893=VERTEX_POINT ( 'NONE', #198749 ) ;
#154909=CARTESIAN_POINT ( 'NONE',  ( -18.38639463286148867, 64.51980042617665845, -194.2731074845244450 ) ) ;
#155363=( BOUNDED_SURFACE ( )  B_SPLINE_SURFACE ( 3, 2, ( 
 ( #230213, #52847, #114105 ),
 ( #33338, #132403, #51540 ),
 ( #131108, #35887, #110258 ),
 ( #111555, #90693, #115393 ) ),
 .UNSPECIFIED., .F., .F., .T. ) 
 B_SPLINE_SURFACE_WITH_KNOTS ( ( 4, 4 ),
 ( 3, 3 ),
 ( 5.727910411845712702, 5.983100554402349225 ),
 ( 0.000000000000000000, 1.000000000000000000 ),
 .UNSPECIFIED. ) 
 GEOMETRIC_REPRESENTATION_ITEM ( )  RATIONAL_B_SPLINE_SURFACE ( (
 ( 1.000000000000000000, 0.8946697475932141597, 1.000000000000000000),
 ( 1.000000000000000000, 0.9035312726220691149, 1.000000000000000000),
 ( 1.000000000000000000, 0.9104333467450248518, 1.000000000000000000),
 ( 1.000000000000000000, 0.9152888060719485130, 1.000000000000000000) ) ) 
 REPRESENTATION_ITEM ( '' )  SURFACE ( )  );
#155450=AXIS2_PLACEMENT_3D ( 'NONE', #84703, #224245, #185131 ) ;
#155486=DIRECTION ( 'NONE',  ( -1.652117596168391700E-15, 1.000000000000000000, 6.982962677686266711E-15 ) ) ;
#155981=( BOUNDED_SURFACE ( )  B_SPLINE_SURFACE ( 3, 2, ( 
 ( #223463, #200070, #164797 ),
 ( #100914, #244311, #205183 ),
 ( #1837, #106068, #81365 ),
 ( #240474, #42284, #30432 ) ),
 .UNSPECIFIED., .F., .F., .F. ) 
 B_SPLINE_SURFACE_WITH_KNOTS ( ( 4, 4 ),
 ( 3, 3 ),
 ( 3.658908243880847788, 4.712388980384689674 ),
 ( 0.000000000000000000, 1.000000000000000000 ),
 .UNSPECIFIED. ) 
 GEOMETRIC_REPRESENTATION_ITEM ( )  RATIONAL_B_SPLINE_SURFACE ( (
 ( 1.000000000000000000, 0.8984936768950640973, 1.000000000000000000),
 ( 1.000000000000000000, 0.8646876308616019413, 1.000000000000000000),
 ( 1.000000000000000000, 0.7953136715913022847, 1.000000000000000000),
 ( 1.000000000000000000, 0.7071067811865475727, 1.000000000000000000) ) ) 
 REPRESENTATION_ITEM ( '' )  SURFACE ( )  );
#156019=VECTOR ( 'NONE', #161563, 1000.000000000000000 ) ;
#156087=EDGE_CURVE ( 'NONE', #73216, #154893, #166452, .T. ) ;
#156134=CARTESIAN_POINT ( 'NONE',  ( -17.01825945287482966, 65.95000000001262208, -190.8731074845244393 ) ) ;
#156173=CARTESIAN_POINT ( 'NONE',  ( -17.11825945287482753, 66.05000000001261640, -190.7731074845244166 ) ) ;
#156175=AXIS2_PLACEMENT_3D ( 'NONE', #212619, #216447, #78219 ) ;
#156455=LINE ( 'NONE', #136843, #215431 ) ;
#156462=DIRECTION ( 'NONE',  ( -1.000000000000000000, 0.000000000000000000, -0.000000000000000000 ) ) ;
#156573=FACE_OUTER_BOUND ( 'NONE', #217002, .T. ) ;
#156802=CARTESIAN_POINT ( 'NONE',  ( -16.88593481969334320, 66.04943990992822478, -182.6712352275799276 ) ) ;
#156875=CARTESIAN_POINT ( 'NONE',  ( 14.77516762759922209, 66.56332574816974557, -188.3462455535252502 ) ) ;
#156995=ORIENTED_EDGE ( 'NONE', *, *, #176150, .T. ) ;
#157078=CARTESIAN_POINT ( 'NONE',  ( -21.65000000000000213, 68.75000000001256240, -182.6731074845244223 ) ) ;
#157258=VERTEX_POINT ( 'NONE', #144286 ) ;
#157427=ORIENTED_EDGE ( 'NONE', *, *, #36511, .T. ) ;
#157535=UNCERTAINTY_MEASURE_WITH_UNIT (LENGTH_MEASURE( 1.000000000000000082E-05 ), #111505, 'distance_accuracy_value', 'NONE');
#157596=LINE ( 'NONE', #196663, #231112 ) ;
#157941=VECTOR ( 'NONE', #501, 1000.000000000000000 ) ;
#157969=CARTESIAN_POINT ( 'NONE',  ( 23.24999999999999645, 70.35000000001261355, -190.8731074845244109 ) ) ;
#157974=ORIENTED_EDGE ( 'NONE', *, *, #188015, .T. ) ;
#158103=CARTESIAN_POINT ( 'NONE',  ( -16.89208623190940273, 66.04842205103706476, -182.6678352813061394 ) ) ;
#158159=PLANE ( 'NONE',  #37527 ) ;
#158174=CARTESIAN_POINT ( 'NONE',  ( 13.76927104934457446, 66.54401276639984530, -188.5115763176266626 ) ) ;
#158192=AXIS2_PLACEMENT_3D ( 'NONE', #144574, #160333, #104161 ) ;
#158350=CARTESIAN_POINT ( 'NONE',  ( -16.94389599338512298, 66.00880201025755412, -190.9154626827142067 ) ) ;
#158533=ORIENTED_EDGE ( 'NONE', *, *, #168561, .F. ) ;
#158590=CARTESIAN_POINT ( 'NONE',  ( 23.04999999999999716, 67.17743825834622839, -194.2731074845244166 ) ) ;
#158878=EDGE_CURVE ( 'NONE', #201172, #13472, #130001, .T. ) ;
#159426=CARTESIAN_POINT ( 'NONE',  ( 15.52844286134409124, 66.62433047358679516, -187.6553174751384745 ) ) ;
#159465=DIRECTION ( 'NONE',  ( -1.073024830501117725E-15, -6.982962677686266711E-15, 1.000000000000000000 ) ) ;
#159511=ORIENTED_EDGE ( 'NONE', *, *, #255913, .T. ) ;
#159589=PLANE ( 'NONE',  #199507 ) ;
#159606=CARTESIAN_POINT ( 'NONE',  ( -16.94445028196808778, 66.00793639031486748, -190.9157773061059800 ) ) ;
#159766=CARTESIAN_POINT ( 'NONE',  ( -16.92570016628982543, 66.04121104227267836, -182.6437581545634146 ) ) ;
#160220=VECTOR ( 'NONE', #70309, 1000.000000000000000 ) ;
#160234=FACE_OUTER_BOUND ( 'NONE', #56893, .T. ) ;
#160333=DIRECTION ( 'NONE',  ( -1.073024830501117725E-15, -6.982962677686266711E-15, 1.000000000000000000 ) ) ;
#160393=CARTESIAN_POINT ( 'NONE',  ( -16.97092634996621996, 65.99911103366474663, -190.8929647182265228 ) ) ;
#160636=CARTESIAN_POINT ( 'NONE',  ( -18.40000000000000213, 70.35000000001261355, -190.8731074845244109 ) ) ;
#160695=CARTESIAN_POINT ( 'NONE',  ( -15.75000000000000355, 66.65000000001258229, -186.7731074845243882 ) ) ;
#160734=EDGE_CURVE ( 'NONE', #74091, #63287, #74667, .T. ) ;
#160738=VERTEX_POINT ( 'NONE', #172492 ) ;
#160855=CARTESIAN_POINT ( 'NONE',  ( -16.94445028196808778, 66.00793639031486748, -190.9157773061059800 ) ) ;
#160883=LINE ( 'NONE', #40948, #217154 ) ;
#160897=EDGE_CURVE ( 'NONE', #127125, #75787, #245263, .T. ) ;
#161028=EDGE_CURVE ( 'NONE', #70737, #74558, #252941, .T. ) ;
#161065=CARTESIAN_POINT ( 'NONE',  ( -17.78043020864321022, 65.14640788800693372, -193.1861566502446408 ) ) ;
#161149=AXIS2_PLACEMENT_3D ( 'NONE', #152960, #112520, #53820 ) ;
#161259=EDGE_CURVE ( 'NONE', #95790, #207406, #187237, .T. ) ;
#161261=DIRECTION ( 'NONE',  ( 1.073024830501117725E-15, 6.982962677686266711E-15, -1.000000000000000000 ) ) ;
#161392=( BOUNDED_CURVE ( )  B_SPLINE_CURVE ( 3, ( #190241, #91130, #170721, #27351 ),
 .UNSPECIFIED., .F., .F. ) 
 B_SPLINE_CURVE_WITH_KNOTS ( ( 4, 4 ),
 ( 3.432212674861197854, 3.693332928900581180 ),
 .UNSPECIFIED. ) 
 CURVE ( )  GEOMETRIC_REPRESENTATION_ITEM ( )  RATIONAL_B_SPLINE_CURVE ( ( 1.000000000000000000, 0.9943260843901262636, 0.9943260843901262636, 1.000000000000000000 ) ) 
 REPRESENTATION_ITEM ( '' )  );
#161502=EDGE_CURVE ( 'NONE', #18319, #104084, #133657, .T. ) ;
#161545=EDGE_CURVE ( 'NONE', #47477, #60767, #240461, .T. ) ;
#161563=DIRECTION ( 'NONE',  ( 1.000000000000000000, 0.000000000000000000, 0.000000000000000000 ) ) ;
#161672=FACE_OUTER_BOUND ( 'NONE', #186645, .T. ) ;
#161680=CARTESIAN_POINT ( 'NONE',  ( -16.89021194854739605, 66.05000000001254534, -182.7805393529200728 ) ) ;
#161710=VECTOR ( 'NONE', #198772, 1000.000000000000000 ) ;
#161776=CARTESIAN_POINT ( 'NONE',  ( 13.77030915526559340, 66.54399267394325079, -185.0344739903776770 ) ) ;
#161833=AXIS2_PLACEMENT_3D ( 'NONE', #70467, #110828, #190395 ) ;
#161892=FACE_OUTER_BOUND ( 'NONE', #254693, .T. ) ;
#161911=ORIENTED_EDGE ( 'NONE', *, *, #53342, .T. ) ;
#162164=LINE ( 'NONE', #63028, #12548 ) ;
#162237=LINE ( 'NONE', #551, #127262 ) ;
#162336=CARTESIAN_POINT ( 'NONE',  ( -16.83233564386387471, 66.06977820342792995, -182.7985868210483318 ) ) ;
#162394=CARTESIAN_POINT ( 'NONE',  ( -15.75000000000000355, 66.15000000001258229, -186.7731074845244166 ) ) ;
#162396=CARTESIAN_POINT ( 'NONE',  ( -15.06774609480957494, 66.58234804117157069, -188.1643200920839547 ) ) ;
#162399=CARTESIAN_POINT ( 'NONE',  ( -16.94445028196807002, 66.00793639031481064, -182.6304376629428816 ) ) ;
#163152=CARTESIAN_POINT ( 'NONE',  ( -17.22361732159832215, 65.65484434141018255, -192.1523229586573223 ) ) ;
#163195=ORIENTED_EDGE ( 'NONE', *, *, #118757, .T. ) ;
#163240=CARTESIAN_POINT ( 'NONE',  ( -12.25000000000000178, 66.65000000001258229, -186.7731074845244166 ) ) ;
#163454=CARTESIAN_POINT ( 'NONE',  ( -16.87036670365549895, 65.91505003675732155, -190.9731074845244336 ) ) ;
#163462=ORIENTED_EDGE ( 'NONE', *, *, #203143, .F. ) ;
#163559=VECTOR ( 'NONE', #163855, 1000.000000000000000 ) ;
#163607=CARTESIAN_POINT ( 'NONE',  ( -16.77308656112215246, 66.05000000001254534, -182.6733006762267451 ) ) ;
#163838=FACE_OUTER_BOUND ( 'NONE', #125225, .T. ) ;
#163855=DIRECTION ( 'NONE',  ( 0.7071067811865463515, 0.7071067811865487940, 4.937700262164540154E-15 ) ) ;
#163950=EDGE_CURVE ( 'NONE', #67839, #232210, #203715, .T. ) ;
#164277=EDGE_LOOP ( 'NONE', ( #42417, #126600, #69979, #218067, #180438 ) ) ;
#164525=CARTESIAN_POINT ( 'NONE',  ( -12.68215100488890634, 66.60336962369484581, -185.6160500917061142 ) ) ;
#164559=DIRECTION ( 'NONE',  ( -1.000000000000000000, 0.000000000000000000, -0.000000000000000000 ) ) ;
#164725=FACE_OUTER_BOUND ( 'NONE', #140648, .T. ) ;
#164797=CARTESIAN_POINT ( 'NONE',  ( -16.93388492042257454, 66.01145817749663536, -182.6225623613382538 ) ) ;
#164920=( GEOMETRIC_REPRESENTATION_CONTEXT ( 3 ) GLOBAL_UNCERTAINTY_ASSIGNED_CONTEXT ( ( #157535 ) ) GLOBAL_UNIT_ASSIGNED_CONTEXT ( ( #111505, #228888, #171508 ) ) REPRESENTATION_CONTEXT ( 'NONE', 'WORKASPACE' ) );
#164950=CARTESIAN_POINT ( 'NONE',  ( -16.93301857435208291, 66.02369064527707110, -182.6373319133629423 ) ) ;
#165345=EDGE_LOOP ( 'NONE', ( #176901, #37927 ) ) ;
#165638=CARTESIAN_POINT ( 'NONE',  ( -16.93589915522259304, 65.99137474131667602, -182.5825473825641438 ) ) ;
#165666=ORIENTED_EDGE ( 'NONE', *, *, #115883, .T. ) ;
#165774=CARTESIAN_POINT ( 'NONE',  ( -16.87683809663750623, 66.05000000001261640, -190.1207434663279230 ) ) ;
#165899=FILL_AREA_STYLE ('',( #105870 ) ) ;
#166155=DIRECTION ( 'NONE',  ( 0.000000000000000000, 6.982962677686266711E-15, -1.000000000000000000 ) ) ;
#166207=CARTESIAN_POINT ( 'NONE',  ( -16.85697194749129224, 66.09145628588886723, -182.9581117521382509 ) ) ;
#166233=VECTOR ( 'NONE', #213183, 1000.000000000000000 ) ;
#166429=LINE ( 'NONE', #63430, #210012 ) ;
#166452=LINE ( 'NONE', #222510, #163559 ) ;
#166508=CARTESIAN_POINT ( 'NONE',  ( -16.77683809663752257, 66.05416425680844839, -190.8591584654202222 ) ) ;
#166773=B_SPLINE_CURVE_WITH_KNOTS ( 'NONE', 3,
 ( #188338, #106208, #130931, #8424, #167519, #69693, #170105, #210478, #247012, #249607 ),
 .UNSPECIFIED., .F., .F.,
 ( 4, 3, 3, 4 ),
 ( 0.000000000000000000, 4.874959354404207151E-05, 9.785140065121151641E-05, 0.0001360444631936073986 ),
 .UNSPECIFIED. ) ;
#166894=VERTEX_POINT ( 'NONE', #149975 ) ;
#166968=LINE ( 'NONE', #10432, #94212 ) ;
#166984=EDGE_LOOP ( 'NONE', ( #77659, #105634, #228648, #139914, #23328 ) ) ;
#167071=CARTESIAN_POINT ( 'NONE',  ( -16.88705144915421030, 66.05000000001261640, -190.5921288898123009 ) ) ;
#167078=ORIENTED_EDGE ( 'NONE', *, *, #226393, .T. ) ;
#167235=CARTESIAN_POINT ( 'NONE',  ( 20.99999999999999645, 66.25000000001256240, -182.6731074845244223 ) ) ;
#167258=CARTESIAN_POINT ( 'NONE',  ( -16.97683809663752186, 66.05000000001257376, -183.4254715027207681 ) ) ;
#167330=EDGE_CURVE ( 'NONE', #216617, #197652, #216013, .T. ) ;
#167479=CARTESIAN_POINT ( 'NONE',  ( -16.85722902420161518, 66.05000000001255955, -182.7886549582941598 ) ) ;
#167519=CARTESIAN_POINT ( 'NONE',  ( -16.86422026484316916, 66.02955263915194450, -190.9408942588514151 ) ) ;
#167538=EDGE_CURVE ( 'NONE', #194460, #60767, #209297, .T. ) ;
#167544=CARTESIAN_POINT ( 'NONE',  ( -12.25000000000000533, 66.65000000001259650, -187.0045385271218379 ) ) ;
#167547=CARTESIAN_POINT ( 'NONE',  ( -16.91776028072577631, 66.03659960638279358, -182.6480834698222964 ) ) ;
#167552=ORIENTED_EDGE ( 'NONE', *, *, #172456, .T. ) ;
#167636=DIRECTION ( 'NONE',  ( 1.000000000000000000, 0.000000000000000000, 0.000000000000000000 ) ) ;
#167805=CARTESIAN_POINT ( 'NONE',  ( -16.79363873026997922, 66.05114977059410819, -182.6769537030789650 ) ) ;
#167878=CARTESIAN_POINT ( 'NONE',  ( 12.25000000000000000, 66.15000000001258229, -186.7731074845244450 ) ) ;
#168149=EDGE_CURVE ( 'NONE', #199921, #4454, #22051, .T. ) ;
#168259=DIRECTION ( 'NONE',  ( 0.000000000000000000, -1.000000000000000000, -6.982962677686266711E-15 ) ) ;
#168339=DIRECTION ( 'NONE',  ( -1.073024830501117725E-15, 6.982962677686266711E-15, -1.000000000000000000 ) ) ;
#168561=EDGE_CURVE ( 'NONE', #242970, #213303, #99947, .T. ) ;
#168634=DIRECTION ( 'NONE',  ( 0.000000000000000000, -1.000000000000000000, -7.759275652592821052E-15 ) ) ;
#168695=DIRECTION ( 'NONE',  ( 1.000000000000000000, 0.000000000000000000, 0.000000000000000000 ) ) ;
#168711=EDGE_CURVE ( 'NONE', #73216, #81857, #123397, .T. ) ;
#168928=AXIS2_PLACEMENT_3D ( 'NONE', #72553, #251150, #152098 ) ;
#169059=COLOUR_RGB ( '', 0.31764706, 0.68627451, 0.89019608) ;
#169229=DIRECTION ( 'NONE',  ( -1.000000000000000000, 0.000000000000000000, -0.000000000000000000 ) ) ;
#169259=CARTESIAN_POINT ( 'NONE',  ( -16.87372386987899020, 66.11939976637583527, -190.3738376126580363 ) ) ;
#169419=LINE ( 'NONE', #248928, #160220 ) ;
#169486=VECTOR ( 'NONE', #197387, 1000.000000000000000 ) ;
#169495=CARTESIAN_POINT ( 'NONE',  ( 12.84435279558019971, 66.58929125296548079, -185.4538990786803083 ) ) ;
#169556=VECTOR ( 'NONE', #120371, 1000.000000000000000 ) ;
#169581=VECTOR ( 'NONE', #5665, 1000.000000000000000 ) ;
#169770=CARTESIAN_POINT ( 'NONE',  ( -16.92570016628985385, 66.04121104227273520, -190.9024568144854470 ) ) ;
#169778=DIRECTION ( 'NONE',  ( 1.073024830501117725E-15, -6.982962677686266711E-15, 1.000000000000000000 ) ) ;
#169837=VERTEX_POINT ( 'NONE', #52729 ) ;
#169848=ORIENTED_EDGE ( 'NONE', *, *, #173222, .F. ) ;
#169923=CARTESIAN_POINT ( 'NONE',  ( -18.40000000000000213, 64.25000000001261924, -190.8731074845244393 ) ) ;
#170094=ORIENTED_EDGE ( 'NONE', *, *, #88365, .F. ) ;
#170105=CARTESIAN_POINT ( 'NONE',  ( -16.87368910959167678, 66.03872618332120226, -190.9106143878838395 ) ) ;
#170171=SHAPE_REPRESENTATION ( 'Snap Open Cable Crossbars 11', ( #2425 ), #185768 ) ;
#170280=CYLINDRICAL_SURFACE ( 'NONE', #133405, 0.9000000000000014655 ) ;
#170680=DIRECTION ( 'NONE',  ( -0.000000000000000000, -6.982962677686266711E-15, 1.000000000000000000 ) ) ;
#170721=CARTESIAN_POINT ( 'NONE',  ( 17.74533788810829904, 65.18150020854172055, -180.3367301594719834 ) ) ;
#170812=CARTESIAN_POINT ( 'NONE',  ( -16.93415306273742260, 66.00437774000003799, -182.6130505421640180 ) ) ;
#170930=DIRECTION ( 'NONE',  ( 0.000000000000000000, 6.982962677686266711E-15, -1.000000000000000000 ) ) ;
#170984=AXIS2_PLACEMENT_3D ( 'NONE', #66216, #205709, #127468 ) ;
#171251=FACE_OUTER_BOUND ( 'NONE', #97297, .T. ) ;
#171427=ORIENTED_EDGE ( 'NONE', *, *, #36968, .T. ) ;
#171508=( NAMED_UNIT ( * ) SI_UNIT ( $, .STERADIAN. ) SOLID_ANGLE_UNIT ( ) );
#171545=LINE ( 'NONE', #172848, #59263 ) ;
#171643=FACE_OUTER_BOUND ( 'NONE', #80227, .T. ) ;
#171779=ORIENTED_EDGE ( 'NONE', *, *, #29248, .F. ) ;
#172079=CARTESIAN_POINT ( 'NONE',  ( -16.94132844910799918, 66.00756324483221249, -182.6269057285421411 ) ) ;
#172367=EDGE_CURVE ( 'NONE', #5245, #196258, #133966, .T. ) ;
#172370=ORIENTED_EDGE ( 'NONE', *, *, #153929, .F. ) ;
#172375=ORIENTED_EDGE ( 'NONE', *, *, #168149, .T. ) ;
#172401=DIRECTION ( 'NONE',  ( -1.000000000000000000, 0.000000000000000000, 0.000000000000000000 ) ) ;
#172456=EDGE_CURVE ( 'NONE', #86769, #228950, #79114, .T. ) ;
#172492=CARTESIAN_POINT ( 'NONE',  ( -16.87331047859649757, 66.05000000001255955, -182.6731074845244223 ) ) ;
#172643=ORIENTED_EDGE ( 'NONE', *, *, #88736, .T. ) ;
#172787=VECTOR ( 'NONE', #17726, 1000.000000000000000 ) ;
#172848=CARTESIAN_POINT ( 'NONE',  ( -16.27683809663750480, 66.65000000001255387, -182.5731074845244279 ) ) ;
#172896=ORIENTED_EDGE ( 'NONE', *, *, #114845, .T. ) ;
#173104=CARTESIAN_POINT ( 'NONE',  ( 21.72449340488910252, 65.71604372252147641, -190.8731074845244393 ) ) ;
#173189=CIRCLE ( 'NONE', #43947, 0.9000000000000014655 ) ;
#173222=EDGE_CURVE ( 'NONE', #193731, #201172, #91350, .T. ) ;
#173516=PRODUCT_CONTEXT ( 'NONE', #145654, 'mechanical' ) ;
#173657=CARTESIAN_POINT ( 'NONE',  ( -18.40000000000000213, 64.25000000001253397, -179.2731074845244450 ) ) ;
#173716=ORIENTED_EDGE ( 'NONE', *, *, #242148, .T. ) ;
#173845=DIRECTION ( 'NONE',  ( 1.000000000000000000, 7.492892343619937423E-30, -1.073024830501117725E-15 ) ) ;
#174050=VECTOR ( 'NONE', #8146, 1000.000000000000000 ) ;
#174663=DIRECTION ( 'NONE',  ( 0.5932847527679299127, 0.8049926720990051576, 4.984624513800587583E-15 ) ) ;
#174728=DIRECTION ( 'NONE',  ( 1.000000000000000000, 0.000000000000000000, 0.000000000000000000 ) ) ;
#174875=EDGE_CURVE ( 'NONE', #252537, #252512, #218318, .T. ) ;
#174973=CYLINDRICAL_SURFACE ( 'NONE', #211348, 0.5000000000000004441 ) ;
#175082=CARTESIAN_POINT ( 'NONE',  ( 18.39999999999999503, 64.25000000001253397, -179.2731074845244450 ) ) ;
#175157=EDGE_CURVE ( 'NONE', #142715, #219313, #36874, .T. ) ;
#175238=CARTESIAN_POINT ( 'NONE',  ( -16.93339986808596720, 65.99489607144667502, -190.9571138127115830 ) ) ;
#175509=ADVANCED_FACE ( 'NONE', ( #185987 ), #124739, .F. ) ;
#175897=EDGE_CURVE ( 'NONE', #195865, #110389, #43610, .T. ) ;
#176150=EDGE_CURVE ( 'NONE', #104084, #76475, #45891, .T. ) ;
#176236=ADVANCED_FACE ( 'NONE', ( #78565 ), #158159, .F. ) ;
#176427=ORIENTED_EDGE ( 'NONE', *, *, #111064, .T. ) ;
#176428=LINE ( 'NONE', #79842, #32334 ) ;
#176444=AXIS2_PLACEMENT_3D ( 'NONE', #158590, #178153, #118155 ) ;
#176570=DIRECTION ( 'NONE',  ( -0.5932847527679299127, -0.8049926720990051576, -6.257843056355997642E-15 ) ) ;
#176757=PLANE ( 'NONE',  #60161 ) ;
#176758=CARTESIAN_POINT ( 'NONE',  ( -18.34374000495059676, 64.52683809665003878, -179.2731074845244450 ) ) ;
#176819=VECTOR ( 'NONE', #27592, 1000.000000000000000 ) ;
#176901=ORIENTED_EDGE ( 'NONE', *, *, #34634, .T. ) ;
#177035=COLOUR_RGB ( '', 0.31764706, 0.68627451, 0.89019608) ;
#177100=AXIS2_PLACEMENT_3D ( 'NONE', #201204, #2991, #202494 ) ;
#177346=CARTESIAN_POINT ( 'NONE',  ( -16.83558968593882099, 66.05000000001261640, -190.8608022969076785 ) ) ;
#177393=CARTESIAN_POINT ( 'NONE',  ( -17.11825945287482753, 66.05000000001260219, -190.8731074845243825 ) ) ;
#177609=CARTESIAN_POINT ( 'NONE',  ( 23.24999999999999645, 67.17743825834622839, -194.2731074845244166 ) ) ;
#177664=CARTESIAN_POINT ( 'NONE',  ( 18.39999999999999503, 70.35000000001261355, -190.8731074845244109 ) ) ;
#177670=B_SPLINE_CURVE_WITH_KNOTS ( 'NONE', 3,
 ( #203472, #27437, #165638, #26123, #105615, #185186, #16835, #53376, #93775, #229451, #170812, #211167, #194192, #32569, #172079, #114631 ),
 .UNSPECIFIED., .F., .F.,
 ( 4, 3, 3, 3, 3, 4 ),
 ( 0.000000000000000000, 1.810570668010599751E-05, 2.740575833570006129E-05, 4.256816319434536945E-05, 5.213463471025743496E-05, 6.641585710718904932E-05 ),
 .UNSPECIFIED. ) ;
#177811=VECTOR ( 'NONE', #12253, 1000.000000000000000 ) ;
#177899=AXIS2_PLACEMENT_3D ( 'NONE', #181605, #159465, #242841 ) ;
#178045=CARTESIAN_POINT ( 'NONE',  ( -17.22361732159831149, 65.65484434141011150, -181.3938920103915677 ) ) ;
#178117=VERTEX_POINT ( 'NONE', #235023 ) ;
#178153=DIRECTION ( 'NONE',  ( 0.000000000000000000, 6.982962677686266711E-15, -1.000000000000000000 ) ) ;
#178359=ORIENTED_EDGE ( 'NONE', *, *, #203143, .T. ) ;
#178700=VERTEX_POINT ( 'NONE', #9885 ) ;
#179001=DIRECTION ( 'NONE',  ( 0.000000000000000000, 0.000000000000000000, -1.000000000000000000 ) ) ;
#179191=CARTESIAN_POINT ( 'NONE',  ( -18.40000000000000213, 67.17743825834611471, -179.2731074845244166 ) ) ;
#179342=CARTESIAN_POINT ( 'NONE',  ( -16.89797118371505036, 66.02361927736811253, -182.5858141169664179 ) ) ;
#179719=DIRECTION ( 'NONE',  ( -1.652117596168391700E-15, 1.000000000000000000, 6.982962677686266711E-15 ) ) ;
#179802=EDGE_CURVE ( 'NONE', #60767, #4454, #149651, .T. ) ;
#179828=FACE_OUTER_BOUND ( 'NONE', #36423, .T. ) ;
#180041=CARTESIAN_POINT ( 'NONE',  ( 15.51872946208853143, 66.62341902196861554, -185.8961612375124446 ) ) ;
#180208=VERTEX_POINT ( 'NONE', #225933 ) ;
#180332=CARTESIAN_POINT ( 'NONE',  ( -16.94180778212363236, 66.00755694428045217, -190.9189239139911649 ) ) ;
#180338=VERTEX_POINT ( 'NONE', #231136 ) ;
#180438=ORIENTED_EDGE ( 'NONE', *, *, #229920, .T. ) ;
#180609=CARTESIAN_POINT ( 'NONE',  ( -16.85718274719425125, 66.02385768539068067, -182.5864538167065518 ) ) ;
#180707=EDGE_CURVE ( 'NONE', #74558, #108824, #90473, .T. ) ;
#181008=DIRECTION ( 'NONE',  ( -0.000000000000000000, -6.982962677686266711E-15, 1.000000000000000000 ) ) ;
#181438=DIRECTION ( 'NONE',  ( 1.000000000000000000, 0.000000000000000000, 0.000000000000000000 ) ) ;
#181527=CARTESIAN_POINT ( 'NONE',  ( -15.15564720441980207, 66.58929125296548079, -185.4538990786802799 ) ) ;
#181593=DIRECTION ( 'NONE',  ( -0.000000000000000000, -6.982962677686266711E-15, 1.000000000000000000 ) ) ;
#181605=CARTESIAN_POINT ( 'NONE',  ( 23.04999999999999716, 67.17743825834619997, -190.8731074845244109 ) ) ;
#181656=FACE_OUTER_BOUND ( 'NONE', #243262, .T. ) ;
#181732=CARTESIAN_POINT ( 'NONE',  ( -16.92132318717937522, 66.03392997600667513, -190.9007008541723565 ) ) ;
#181941=CARTESIAN_POINT ( 'NONE',  ( -16.89020380669786192, 66.05000000001261640, -190.7656963364138676 ) ) ;
#181949=CARTESIAN_POINT ( 'NONE',  ( -15.75000000000000355, 66.65000000001258229, -186.7731074845243882 ) ) ;
#181975=ORIENTED_EDGE ( 'NONE', *, *, #11425, .T. ) ;
#182565=CARTESIAN_POINT ( 'NONE',  ( -16.86379686415369150, 66.02478224075939295, -182.5897175954341662 ) ) ;
#182603=CARTESIAN_POINT ( 'NONE',  ( 18.39999999999999503, 64.52683809665005299, -182.6731074845244507 ) ) ;
#183124=CARTESIAN_POINT ( 'NONE',  ( 18.39999999999999503, 70.35000000001254250, -179.2731074845243882 ) ) ;
#183249=CARTESIAN_POINT ( 'NONE',  ( -18.41431012584568805, 64.51252797080434220, -179.2498714714227503 ) ) ;
#183376=CARTESIAN_POINT ( 'NONE',  ( -18.40000000000000213, 64.52683809665012404, -190.8731074845244393 ) ) ;
#183425=B_SPLINE_CURVE_WITH_KNOTS ( 'NONE', 3,
 ( #163240, #184068, #118979, #5401, #79812, #84932, #23750, #2848, #164525, #40750, #244035, #64129, #121570, #143655, #1568, #81103, #223186, #120289, #202352, #219337, #181527, #21182, #39466, #238918, #82371, #240210, #65404, #198497, #19882, #160695 ),
 .UNSPECIFIED., .F., .F.,
 ( 4, 2, 2, 2, 2, 2, 2, 2, 2, 2, 2, 2, 2, 2, 4 ),
 ( 0.000000000000000000, 0.0003422764154113552447, 0.0006845528308227104893, 0.001026829246234065842, 0.001369105661645420979, 0.002053658492468075740, 0.002738211323290730068, 0.003080487738702054629, 0.003422764154113380058, 0.003765040569524704620, 0.004107316984936030049, 0.004449593400347354177, 0.004791869815758679173, 0.005134146231170004168, 0.005476422646581329164 ),
 .UNSPECIFIED. ) ;
#183525=PLANE ( 'NONE',  #115728 ) ;
#183789=CARTESIAN_POINT ( 'NONE',  ( -16.81744102076748959, 66.05000000001255955, -182.6731074845244223 ) ) ;
#184068=CARTESIAN_POINT ( 'NONE',  ( -12.25000000000000178, 66.65000000001258229, -186.6573643172504831 ) ) ;
#184267=DIRECTION ( 'NONE',  ( 0.7071067811865463515, -0.7071067811865487940, -5.696443396193425170E-15 ) ) ;
#184494=CARTESIAN_POINT ( 'NONE',  ( -13.77178122865955068, 66.54397173950466993, -188.5119094494586705 ) ) ;
#185109=ORIENTED_EDGE ( 'NONE', *, *, #189710, .T. ) ;
#185131=DIRECTION ( 'NONE',  ( 0.000000000000000000, -6.789366196018718420E-15, 1.000000000000000000 ) ) ;
#185186=CARTESIAN_POINT ( 'NONE',  ( -16.93294127766158752, 65.99671989705768738, -182.5932002186951877 ) ) ;
#185227=ORIENTED_EDGE ( 'NONE', *, *, #242240, .T. ) ;
#185267=DIRECTION ( 'NONE',  ( 0.7071067811865214825, -0.7071067811865735520, 0.000000000000000000 ) ) ;
#185341=CARTESIAN_POINT ( 'NONE',  ( -23.25000000000000355, 70.35000000001264198, -194.2731074845243882 ) ) ;
#185372=ADVANCED_FACE ( 'NONE', ( #225305 ), #244888, .F. ) ;
#185454=AXIS2_PLACEMENT_3D ( 'NONE', #151694, #31747, #173845 ) ;
#185768=( GEOMETRIC_REPRESENTATION_CONTEXT ( 3 ) GLOBAL_UNCERTAINTY_ASSIGNED_CONTEXT ( ( #196607 ) ) GLOBAL_UNIT_ASSIGNED_CONTEXT ( ( #185899, #12427, #129775 ) ) REPRESENTATION_CONTEXT ( 'NONE', 'WORKASPACE' ) );
#185899=( LENGTH_UNIT ( ) NAMED_UNIT ( * ) SI_UNIT ( .MILLI., .METRE. ) );
#185965=EDGE_LOOP ( 'NONE', ( #7717, #31526, #58794, #104367, #143955, #148285, #229410, #114234, #90435 ) ) ;
#185987=FACE_OUTER_BOUND ( 'NONE', #137261, .T. ) ;
#186128=LINE ( 'NONE', #167878, #97539 ) ;
#186351=CYLINDRICAL_SURFACE ( 'NONE', #72440, 0.1999999999999987899 ) ;
#186545=CARTESIAN_POINT ( 'NONE',  ( 16.27683809663749770, 66.65000000001263913, -194.2731074845244166 ) ) ;
#186566=CARTESIAN_POINT ( 'NONE',  ( -15.55912972643741199, 67.50912972645004118, -190.9731074845244336 ) ) ;
#186615=CARTESIAN_POINT ( 'NONE',  ( -16.97683810757273193, 66.05000000001261640, -190.2595307720632150 ) ) ;
#186645=EDGE_LOOP ( 'NONE', ( #88018, #38654, #141750, #130938, #38642 ) ) ;
#186695=ORIENTED_EDGE ( 'NONE', *, *, #83131, .T. ) ;
#187044=CARTESIAN_POINT ( 'NONE',  ( -16.89155683852770551, 66.05000000001524540, -183.3004793340630556 ) ) ;
#187107=CARTESIAN_POINT ( 'NONE',  ( -16.94165728009536664, 66.01213024408876606, -182.6320524760142234 ) ) ;
#187131=AXIS2_PLACEMENT_3D ( 'NONE', #61311, #198244, #19626 ) ;
#187237=LINE ( 'NONE', #32017, #228186 ) ;
#187300=CARTESIAN_POINT ( 'NONE',  ( 18.54999999999999716, 66.05000000001260219, -190.8731074845244962 ) ) ;
#187313=ORIENTED_EDGE ( 'NONE', *, *, #214522, .T. ) ;
#187378=ORIENTED_EDGE ( 'NONE', *, *, #254181, .F. ) ;
#187413=ADVANCED_FACE ( 'NONE', ( #94243 ), #92961, .F. ) ;
#187577=DIRECTION ( 'NONE',  ( 0.5932847527679310229, 0.8049926720990042694, 6.257843056355992909E-15 ) ) ;
#187750=CARTESIAN_POINT ( 'NONE',  ( 12.30626653967341610, 66.64320997496669463, -186.3182809759104543 ) ) ;
#187861=LINE ( 'NONE', #48324, #65409 ) ;
#187862=EDGE_CURVE ( 'NONE', #103692, #250290, #51636, .T. ) ;
#187896=CARTESIAN_POINT ( 'NONE',  ( -16.85697194749126382, 66.09145628588898091, -190.5881032169105822 ) ) ;
#188015=EDGE_CURVE ( 'NONE', #142715, #108824, #243390, .T. ) ;
#188048=EDGE_CURVE ( 'NONE', #26389, #38279, #25638, .T. ) ;
#188119=B_SPLINE_CURVE_WITH_KNOTS ( 'NONE', 3,
 ( #56501, #78638, #180332, #95640, #139893, #96895, #218144, #77357, #199908, #198596, #60367, #197307, #38257, #175238, #39569, #119078, #40847, #81199, #235170 ),
 .UNSPECIFIED., .F., .F.,
 ( 4, 3, 3, 3, 3, 3, 4 ),
 ( 0.0001624081864585794055, 0.0001685232196531677375, 0.0001764526673566770378, 0.0001916878551483278104, 0.0002009890782182702088, 0.0002238845907555191150, 0.0002283406619926350520 ),
 .UNSPECIFIED. ) ;
#188160=DIRECTION ( 'NONE',  ( -1.020425574104004196E-15, -6.982962677686266711E-15, 1.000000000000000000 ) ) ;
#188207=CARTESIAN_POINT ( 'NONE',  ( 23.04999999999999716, 67.17743825834611471, -179.2731074845244166 ) ) ;
#188338=CARTESIAN_POINT ( 'NONE',  ( -16.87036670365549895, 66.01058118071095748, -191.0026676018264880 ) ) ;
#188385=VERTEX_POINT ( 'NONE', #20205 ) ;
#188697=AXIS2_PLACEMENT_3D ( 'NONE', #2846, #242745, #26290 ) ;
#189018=CARTESIAN_POINT ( 'NONE',  ( 12.42718393586867265, 66.62934494888909853, -185.9972842285435490 ) ) ;
#189301=CARTESIAN_POINT ( 'NONE',  ( -16.94878442675512886, 66.00827089702160322, -190.9113270601623071 ) ) ;
#189350=CARTESIAN_POINT ( 'NONE',  ( -21.65000000000000213, 68.75000000001261924, -190.8731074845244109 ) ) ;
#189710=EDGE_CURVE ( 'NONE', #207406, #79239, #149195, .T. ) ;
#189908=CARTESIAN_POINT ( 'NONE',  ( -16.77779411440718249, 66.05389855290493983, -182.6861649015289402 ) ) ;
#190241=CARTESIAN_POINT ( 'NONE',  ( 16.87683809663749557, 66.05000000001257376, -182.6731074845244223 ) ) ;
#190260=DIRECTION ( 'NONE',  ( 1.186688945009009831E-16, 1.000000000000000000, 6.982962677686266711E-15 ) ) ;
#190395=DIRECTION ( 'NONE',  ( 1.000000000000000000, 0.000000000000000000, 0.000000000000000000 ) ) ;
#190605=DIRECTION ( 'NONE',  ( 1.000000000000000000, -1.541976423090492636E-14, 0.000000000000000000 ) ) ;
#190869=CARTESIAN_POINT ( 'NONE',  ( -16.88815647973233780, 66.04916738069687199, -190.8758904211984202 ) ) ;
#190941=ORIENTED_EDGE ( 'NONE', *, *, #195783, .F. ) ;
#190960=CARTESIAN_POINT ( 'NONE',  ( -12.29659703204452015, 66.64411154551000038, -187.2344645877464018 ) ) ;
#190977=LINE ( 'NONE', #157969, #98057 ) ;
#191121=FACE_OUTER_BOUND ( 'NONE', #27472, .T. ) ;
#191207=CARTESIAN_POINT ( 'NONE',  ( -16.77779411503079388, 66.05389855308847302, -190.8600500669045914 ) ) ;
#191277=ORIENTED_EDGE ( 'NONE', *, *, #161259, .F. ) ;
#191363=VECTOR ( 'NONE', #191804, 1000.000000000000000 ) ;
#191561=DIRECTION ( 'NONE',  ( 1.000000000000000000, 0.000000000000000000, 0.000000000000000000 ) ) ;
#191562=CARTESIAN_POINT ( 'NONE',  ( -17.11825945287481332, 66.05000000001255955, -182.7731074845244450 ) ) ;
#191653=CARTESIAN_POINT ( 'NONE',  ( 18.39999999999999503, 64.52683809665012404, -190.8731074845244393 ) ) ;
#191707=CARTESIAN_POINT ( 'NONE',  ( -16.81931177881022066, 66.06300394050866487, -182.7498896059072422 ) ) ;
#191757=AXIS2_PLACEMENT_3D ( 'NONE', #44637, #181593, #45915 ) ;
#191804=DIRECTION ( 'NONE',  ( -0.000000000000000000, 6.982962677686266711E-15, -1.000000000000000000 ) ) ;
#191964=ORIENTED_EDGE ( 'NONE', *, *, #29248, .T. ) ;
#192379=DIRECTION ( 'NONE',  ( 0.5932847527679310229, 0.8049926720990042694, 5.621233785078285907E-15 ) ) ;
#192680=DIRECTION ( 'NONE',  ( 0.000000000000000000, -1.000000000000000000, -6.982962677686266711E-15 ) ) ;
#192901=CARTESIAN_POINT ( 'NONE',  ( -18.39999999999999858, 64.52683809665015247, -194.2232782360584622 ) ) ;
#192933=ORIENTED_EDGE ( 'NONE', *, *, #230937, .T. ) ;
#192966=CARTESIAN_POINT ( 'NONE',  ( -16.87683809663752399, 66.15000000001255387, -183.4254715027207396 ) ) ;
#193158=CARTESIAN_POINT ( 'NONE',  ( -16.85718274719454257, 66.02385768539078015, -190.9597611523421392 ) ) ;
#193218=ORIENTED_EDGE ( 'NONE', *, *, #11161, .F. ) ;
#193513=DIRECTION ( 'NONE',  ( 1.000000000000000000, 0.000000000000000000, 0.000000000000000000 ) ) ;
#193731=VERTEX_POINT ( 'NONE', #121515 ) ;
#194153=LINE ( 'NONE', #250252, #72844 ) ;
#194159=FACE_OUTER_BOUND ( 'NONE', #226610, .T. ) ;
#194192=CARTESIAN_POINT ( 'NONE',  ( -16.93658211146644987, 66.00589133767134342, -182.6188124145687652 ) ) ;
#194252=CARTESIAN_POINT ( 'NONE',  ( 18.39999999999999503, 67.17743825834611471, -179.2731074845244166 ) ) ;
#194297=DIRECTION ( 'NONE',  ( 1.000000000000000000, 0.000000000000000000, 0.000000000000000000 ) ) ;
#194460=VERTEX_POINT ( 'NONE', #35903 ) ;
#194476=CIRCLE ( 'NONE', #177899, 0.1999999999999987899 ) ;
#194584=VERTEX_POINT ( 'NONE', #72007 ) ;
#194713=CARTESIAN_POINT ( 'NONE',  ( 13.43443725621851570, 66.55344247694002036, -188.4331655301785133 ) ) ;
#194946=CARTESIAN_POINT ( 'NONE',  ( -15.55912972643741199, 67.50912972645004118, -190.8731074845244109 ) ) ;
#195024=ORIENTED_EDGE ( 'NONE', *, *, #237643, .T. ) ;
#195201=CARTESIAN_POINT ( 'NONE',  ( -21.65000000000000213, 68.75000000001256240, -182.6731074845244223 ) ) ;
#195269=PLANE ( 'NONE',  #220924 ) ;
#195308=ORIENTED_EDGE ( 'NONE', *, *, #236501, .F. ) ;
#195449=CARTESIAN_POINT ( 'NONE',  ( -21.64999999999999858, 65.95000000001255103, -182.6731074845244223 ) ) ;
#195656=ORIENTED_EDGE ( 'NONE', *, *, #238438, .T. ) ;
#195749=ORIENTED_EDGE ( 'NONE', *, *, #36511, .F. ) ;
#195783=EDGE_CURVE ( 'NONE', #166894, #23645, #72204, .T. ) ;
#195865=VERTEX_POINT ( 'NONE', #40748 ) ;
#196015=VECTOR ( 'NONE', #234359, 1000.000000000000000 ) ;
#196153=AXIS2_PLACEMENT_3D ( 'NONE', #46192, #24100, #141442 ) ;
#196258=VERTEX_POINT ( 'NONE', #187300 ) ;
#196294=CARTESIAN_POINT ( 'NONE',  ( -18.40000000000000213, 70.35000000001261355, -190.8731074845244109 ) ) ;
#196607=UNCERTAINTY_MEASURE_WITH_UNIT (LENGTH_MEASURE( 1.000000000000000082E-05 ), #185899, 'distance_accuracy_value', 'NONE');
#196613=PLANE ( 'NONE',  #1263 ) ;
#196663=CARTESIAN_POINT ( 'NONE',  ( -16.77683809663752257, 66.05000000001255955, -182.6731074845244223 ) ) ;
#196935=CARTESIAN_POINT ( 'NONE',  ( -20.65000000000000568, 68.75000000001261924, -190.8731074845244109 ) ) ;
#197052=CARTESIAN_POINT ( 'NONE',  ( -23.25000000000000355, 64.25000000001264766, -194.2731074845244450 ) ) ;
#197171=EDGE_LOOP ( 'NONE', ( #7529, #68212, #215494 ) ) ;
#197307=CARTESIAN_POINT ( 'NONE',  ( -16.93230518875208190, 65.99924963859275806, -190.9473291364229226 ) ) ;
#197387=DIRECTION ( 'NONE',  ( 0.000000000000000000, -1.000000000000000000, -6.982962677686266711E-15 ) ) ;
#197428=LINE ( 'NONE', #179191, #157941 ) ;
#197588=FACE_OUTER_BOUND ( 'NONE', #116811, .T. ) ;
#197652=VERTEX_POINT ( 'NONE', #5787 ) ;
#197830=AXIS2_PLACEMENT_3D ( 'NONE', #243725, #50636, #130180 ) ;
#198004=ORIENTED_EDGE ( 'NONE', *, *, #175897, .F. ) ;
#198047=MANIFOLD_SOLID_BREP ( 'Stock-MAS-200-1', #203301 ) ;
#198244=DIRECTION ( 'NONE',  ( 1.186688945009009831E-16, 1.000000000000000000, 6.982962677686266711E-15 ) ) ;
#198497=CARTESIAN_POINT ( 'NONE',  ( -15.73854595235690468, 66.64858632091116419, -186.5427639169753888 ) ) ;
#198531=CARTESIAN_POINT ( 'NONE',  ( 12.24999999999999822, 66.65000000001258229, -187.0015881126993520 ) ) ;
#198596=CARTESIAN_POINT ( 'NONE',  ( -16.93255653858138388, 66.00154854603545118, -190.9414641165347462 ) ) ;
#198749=CARTESIAN_POINT ( 'NONE',  ( -16.94107738177415712, 65.98576071487597972, -190.9731074845244336 ) ) ;
#198772=DIRECTION ( 'NONE',  ( -0.000000000000000000, -6.982962677686266711E-15, 1.000000000000000000 ) ) ;
#198816=CARTESIAN_POINT ( 'NONE',  ( -18.40000000000000213, 64.52132590001262713, -179.2978007008650536 ) ) ;
#198883=ORIENTED_EDGE ( 'NONE', *, *, #153929, .T. ) ;
#199128=EDGE_CURVE ( 'NONE', #95790, #49183, #67956, .T. ) ;
#199193=FACE_OUTER_BOUND ( 'NONE', #210311, .T. ) ;
#199312=ADVANCED_FACE ( 'NONE', ( #133076 ), #136918, .F. ) ;
#199404=ORIENTED_EDGE ( 'NONE', *, *, #168149, .F. ) ;
#199507=AXIS2_PLACEMENT_3D ( 'NONE', #125588, #63037, #43494 ) ;
#199569=ADVANCED_FACE ( 'NONE', ( #85897 ), #70257, .F. ) ;
#199576=EDGE_LOOP ( 'NONE', ( #33851, #57487, #8492, #80679 ) ) ;
#199607=VECTOR ( 'NONE', #187577, 1000.000000000000000 ) ;
#199620=CARTESIAN_POINT ( 'NONE',  ( 15.66039659514496130, 66.63925083009746686, -186.2085373439172145 ) ) ;
#199626=VERTEX_POINT ( 'NONE', #136592 ) ;
#199658=ORIENTED_EDGE ( 'NONE', *, *, #146910, .F. ) ;
#199720=CARTESIAN_POINT ( 'NONE',  ( -18.34374000495060386, 64.52683809665015247, -194.2731074845244450 ) ) ;
#199786=DIRECTION ( 'NONE',  ( 0.000000000000000000, -1.000000000000000000, -6.982962677686266711E-15 ) ) ;
#199844=CARTESIAN_POINT ( 'NONE',  ( 15.75000000000000355, 66.65000000001258229, -187.0045385271217526 ) ) ;
#199907=AXIS2_PLACEMENT_3D ( 'NONE', #233208, #136630, #234450 ) ;
#199908=CARTESIAN_POINT ( 'NONE',  ( -16.93302609847409457, 66.00331747920938597, -190.9367189891619034 ) ) ;
#199921=VERTEX_POINT ( 'NONE', #6071 ) ;
#199944=CYLINDRICAL_SURFACE ( 'NONE', #177100, 0.1000000000000050432 ) ;
#200043=CARTESIAN_POINT ( 'NONE',  ( -18.40000000000000213, 64.52683809665003878, -179.3490535513324176 ) ) ;
#200070=CARTESIAN_POINT ( 'NONE',  ( -16.91049119928362643, 66.05000000001255955, -182.6413870913335700 ) ) ;
#200071=CARTESIAN_POINT ( 'NONE',  ( 20.05000000000002913, 68.75000000001260503, -194.2731074845244166 ) ) ;
#200333=ORIENTED_EDGE ( 'NONE', *, *, #11076, .F. ) ;
#200422=CARTESIAN_POINT ( 'NONE',  ( 15.48841904831874849, 67.43841904833138301, -190.8731074845244393 ) ) ;
#200783=CARTESIAN_POINT ( 'NONE',  ( -16.97048361161167307, 66.05000000001257376, -183.1642231400940375 ) ) ;
#200999=DIRECTION ( 'NONE',  ( -1.000000000000000000, 1.646408749285562691E-14, 1.149681084847720908E-28 ) ) ;
#201116=ADVANCED_FACE ( 'NONE', ( #197588 ), #70708, .T. ) ;
#201172=VERTEX_POINT ( 'NONE', #22843 ) ;
#201204=CARTESIAN_POINT ( 'NONE',  ( -15.55912972643740488, 67.50912972644997012, -182.5731074845244279 ) ) ;
#201287=DIRECTION ( 'NONE',  ( 0.2834754621636439431, 0.2834754621636471628, 0.9161240771326858434 ) ) ;
#201462=CARTESIAN_POINT ( 'NONE',  ( -18.40000000000000213, 64.51332499825495859, -194.2731074845244450 ) ) ;
#201463=ORIENTED_EDGE ( 'NONE', *, *, #195783, .T. ) ;
#201486=CARTESIAN_POINT ( 'NONE',  ( -16.97683809663753252, 66.05000000001263061, -190.2515827158545392 ) ) ;
#201538=CARTESIAN_POINT ( 'NONE',  ( -18.40000000000000213, 64.52683809665012404, -190.9731074845244621 ) ) ;
#202064=CARTESIAN_POINT ( 'NONE',  ( -16.87242674293850087, 66.05000000001263061, -190.8741977308967819 ) ) ;
#202113=CARTESIAN_POINT ( 'NONE',  ( -16.86733706339143879, 66.03400947037287949, -182.6199921825257206 ) ) ;
#202133=CARTESIAN_POINT ( 'NONE',  ( -14.00000000000000178, 66.15000000001258229, -186.7731074845244166 ) ) ;
#202164=CARTESIAN_POINT ( 'NONE',  ( 14.22916352759893677, 66.54258906972242471, -185.0231915757782133 ) ) ;
#202352=CARTESIAN_POINT ( 'NONE',  ( -14.87770893841225650, 66.56936289831583053, -185.2548468664635379 ) ) ;
#202438=LINE ( 'NONE', #85024, #169556 ) ;
#202494=DIRECTION ( 'NONE',  ( -0.7071067811865301422, 0.7071067811865648922, 0.000000000000000000 ) ) ;
#202519=( BOUNDED_CURVE ( )  B_SPLINE_CURVE ( 3, ( #60342, #237714, #218122, #119057 ),
 .UNSPECIFIED., .F., .F. ) 
 B_SPLINE_CURVE_WITH_KNOTS ( ( 4, 4 ),
 ( -9.769962616701377556E-15, 1.570796326794891673 ),
 .UNSPECIFIED. ) 
 CURVE ( )  GEOMETRIC_REPRESENTATION_ITEM ( )  RATIONAL_B_SPLINE_CURVE ( ( 1.000000000000000000, 0.8047378541243637162, 0.8047378541243637162, 1.000000000000000000 ) ) 
 REPRESENTATION_ITEM ( '' )  );
#202718=CARTESIAN_POINT ( 'NONE',  ( -16.80891096016306463, 66.05000000001255955, -182.6554446772547635 ) ) ;
#202730=CARTESIAN_POINT ( 'NONE',  ( -16.89318236219974523, 66.04846474213741203, -182.6679778524186020 ) ) ;
#202740=ADVANCED_FACE ( 'NONE', ( #164725 ), #159589, .F. ) ;
#202786=CARTESIAN_POINT ( 'NONE',  ( -12.84409460144756743, 66.58931770574463371, -188.0919640425761372 ) ) ;
#202826=CARTESIAN_POINT ( 'NONE',  ( -18.40000000000000213, 64.58541674041282477, -190.8731074845244393 ) ) ;
#202832=DIRECTION ( 'NONE',  ( -1.000000000000000000, 0.000000000000000000, 0.000000000000000000 ) ) ;
#203129=ORIENTED_EDGE ( 'NONE', *, *, #87891, .F. ) ;
#203132=EDGE_LOOP ( 'NONE', ( #254377, #209376, #35981, #99002 ) ) ;
#203143=EDGE_CURVE ( 'NONE', #250290, #188385, #52378, .T. ) ;
#203301=CLOSED_SHELL ( 'NONE', ( #62779, #175509, #246791, #116509, #238278, #220421, #47886, #234474, #112767, #176236, #17680, #207163, #83177, #202740, #44386, #10463, #224795, #256384, #152797, #23961, #112257, #72135, #45577, #247430, #226560, #101915, #187413, #12601, #199569, #251414, #61472, #98748, #255427, #62784, #185372, #128223, #138787, #199312, #243368, #88551, #83276, #72666, #11432, #78647, #228088, #19571, #984, #6125, #136194, #124458, #201116, #238245, #47302 ) ) ;
#203386=EDGE_CURVE ( 'NONE', #180208, #78167, #101199, .T. ) ;
#203457=EDGE_LOOP ( 'NONE', ( #207555, #11926, #117343, #117149 ) ) ;
#203472=CARTESIAN_POINT ( 'NONE',  ( -16.94107738177414291, 65.98576071487592287, -182.5731074845244279 ) ) ;
#203479=ORIENTED_EDGE ( 'NONE', *, *, #244517, .T. ) ;
#203715=LINE ( 'NONE', #238995, #229465 ) ;
#204005=CARTESIAN_POINT ( 'NONE',  ( -16.97683810757273193, 66.05000000001255955, -183.2866841969855614 ) ) ;
#204062=CARTESIAN_POINT ( 'NONE',  ( -15.39946565075091200, 66.61046543766590844, -187.8482981801344920 ) ) ;
#204063=CARTESIAN_POINT ( 'NONE',  ( 23.24999999999999645, 70.35000000001255671, -182.6731074845243938 ) ) ;
#204158=EDGE_LOOP ( 'NONE', ( #94951, #230780, #216883, #212420 ) ) ;
#204512=ORIENTED_EDGE ( 'NONE', *, *, #168561, .T. ) ;
#204561=CARTESIAN_POINT ( 'NONE',  ( 18.54999999999999716, 67.25000000001257661, -190.8731074845244109 ) ) ;
#204565=EDGE_CURVE ( 'NONE', #92187, #239104, #58153, .T. ) ;
#204750=( BOUNDED_SURFACE ( )  B_SPLINE_SURFACE ( 3, 2, ( 
 ( #239368, #140239, #21613 ),
 ( #60706, #43732, #120727 ),
 ( #22912, #80249, #124565 ),
 ( #142801, #183249, #20338 ) ),
 .UNSPECIFIED., .F., .F., .F. ) 
 B_SPLINE_SURFACE_WITH_KNOTS ( ( 4, 4 ),
 ( 3, 3 ),
 ( 0.3000847527772363410, 0.5552748953338753068 ),
 ( 0.000000000000000000, 1.000000000000000000 ),
 .UNSPECIFIED. ) 
 GEOMETRIC_REPRESENTATION_ITEM ( )  RATIONAL_B_SPLINE_SURFACE ( (
 ( 1.000000000000000000, 0.9152888060719485130, 1.000000000000000000),
 ( 1.000000000000000000, 0.9104333467450282935, 1.000000000000000000),
 ( 1.000000000000000000, 0.9035312726220630086, 1.000000000000000000),
 ( 1.000000000000000000, 0.8946697475932141597, 1.000000000000000000) ) ) 
 REPRESENTATION_ITEM ( '' )  SURFACE ( )  );
#205183=CARTESIAN_POINT ( 'NONE',  ( -16.97092634996622706, 65.99911103366466136, -182.6532502508223104 ) ) ;
#205271=EDGE_LOOP ( 'NONE', ( #38876, #249101, #132993, #163462, #250320 ) ) ;
#205398=VECTOR ( 'NONE', #193513, 1000.000000000000000 ) ;
#205503=ORIENTED_EDGE ( 'NONE', *, *, #204565, .F. ) ;
#205533=AXIS2_PLACEMENT_3D ( 'NONE', #64167, #164559, #244073 ) ;
#205709=DIRECTION ( 'NONE',  ( 0.000000000000000000, 1.000000000000000000, 6.982962677686266711E-15 ) ) ;
#205733=ORIENTED_EDGE ( 'NONE', *, *, #10899, .F. ) ;
#205832=EDGE_CURVE ( 'NONE', #76104, #235005, #56395, .T. ) ;
#205861=ORIENTED_EDGE ( 'NONE', *, *, #124749, .T. ) ;
#205939=VERTEX_POINT ( 'NONE', #4135 ) ;
#206099=FACE_OUTER_BOUND ( 'NONE', #197171, .T. ) ;
#206116=ORIENTED_EDGE ( 'NONE', *, *, #67633, .T. ) ;
#206128=DIRECTION ( 'NONE',  ( -1.000000000000000000, 0.000000000000000000, 0.000000000000000000 ) ) ;
#206267=CARTESIAN_POINT ( 'NONE',  ( 18.39999999999998082, 64.52683809665015247, -194.2731074845244450 ) ) ;
#206346=LINE ( 'NONE', #189350, #120064 ) ;
#206572=CIRCLE ( 'NONE', #40011, 1.500000000000001332 ) ;
#206579=CARTESIAN_POINT ( 'NONE',  ( -16.97683809663752186, 66.05000000001255955, -183.4254715027207396 ) ) ;
#206609=VECTOR ( 'NONE', #251236, 1000.000000000000000 ) ;
#206659=VECTOR ( 'NONE', #85562, 1000.000000000000000 ) ;
#206763=EDGE_CURVE ( 'NONE', #125626, #208807, #6343, .T. ) ;
#206890=CARTESIAN_POINT ( 'NONE',  ( -16.79814274880124358, 66.05072745733529871, -190.8706744474764321 ) ) ;
#206902=EDGE_CURVE ( 'NONE', #6267, #221894, #18812, .T. ) ;
#207058=DIRECTION ( 'NONE',  ( 1.000000000000000000, 0.000000000000000000, 0.000000000000000000 ) ) ;
#207099=AXIS2_PLACEMENT_3D ( 'NONE', #146540, #110000, #145263 ) ;
#207127=LINE ( 'NONE', #28527, #199607 ) ;
#207163=ADVANCED_FACE ( 'NONE', ( #156573 ), #254327, .F. ) ;
#207264=CARTESIAN_POINT ( 'NONE',  ( -16.89268316805465986, 66.04827818677036078, -182.6673550059788909 ) ) ;
#207406=VERTEX_POINT ( 'NONE', #67702 ) ;
#207462=CARTESIAN_POINT ( 'NONE',  ( -16.89935556175704789, 66.05000000001261640, -190.3834311216385515 ) ) ;
#207555=ORIENTED_EDGE ( 'NONE', *, *, #7513, .T. ) ;
#207562=LINE ( 'NONE', #148871, #227309 ) ;
#207642=CARTESIAN_POINT ( 'NONE',  ( -33.72168855820452649, 64.52683809665015247, -194.2731074845244450 ) ) ;
#207849=DIRECTION ( 'NONE',  ( 1.186688945009010077E-16, 1.000000000000000000, 6.982962677686266711E-15 ) ) ;
#208115=CIRCLE ( 'NONE', #153986, 0.1999999999999987899 ) ;
#208678=EDGE_CURVE ( 'NONE', #54689, #205939, #166429, .T. ) ;
#208700=CARTESIAN_POINT ( 'NONE',  ( 17.74533788810831325, 65.18150020854182003, -193.2094848095768782 ) ) ;
#208747=CARTESIAN_POINT ( 'NONE',  ( -16.84981964351500139, 66.08268176591401755, -190.6535058705039773 ) ) ;
#208807=VERTEX_POINT ( 'NONE', #35171 ) ;
#209216=ORIENTED_EDGE ( 'NONE', *, *, #74804, .F. ) ;
#209273=CARTESIAN_POINT ( 'NONE',  ( 18.39999999999999503, 70.35000000001261355, -190.8731074845244109 ) ) ;
#209297=LINE ( 'NONE', #50210, #105121 ) ;
#209376=ORIENTED_EDGE ( 'NONE', *, *, #10195, .T. ) ;
#209449=CARTESIAN_POINT ( 'NONE',  ( -16.77902162784673479, 66.05358074280475478, -190.8611162404550896 ) ) ;
#209527=CARTESIAN_POINT ( 'NONE',  ( -18.39999999999999858, 64.25000000001264766, -194.2731074845244450 ) ) ;
#209587=DIRECTION ( 'NONE',  ( 0.000000000000000000, -1.000000000000000000, -6.982962677686266711E-15 ) ) ;
#209629=CARTESIAN_POINT ( 'NONE',  ( -16.87683809663752399, 66.15000000001259650, -190.1207434663281219 ) ) ;
#209697=AXIS2_PLACEMENT_3D ( 'NONE', #186566, #28811, #185267 ) ;
#209966=DIRECTION ( 'NONE',  ( -0.7071067811865487940, -0.7071067811865463515, -4.216150419019404490E-15 ) ) ;
#210012=VECTOR ( 'NONE', #223783, 1000.000000000000000 ) ;
#210026=EDGE_CURVE ( 'NONE', #208807, #178117, #235932, .T. ) ;
#210161=CARTESIAN_POINT ( 'NONE',  ( 20.99999999999999645, 66.25000000001256240, -182.6731074845244223 ) ) ;
#210231=EDGE_LOOP ( 'NONE', ( #92266, #169848, #57844, #106850 ) ) ;
#210311=EDGE_LOOP ( 'NONE', ( #3609, #220764, #172896, #239415 ) ) ;
#210425=ORIENTED_EDGE ( 'NONE', *, *, #213915, .T. ) ;
#210478=CARTESIAN_POINT ( 'NONE',  ( -16.87845715379269507, 66.04214188611558711, -190.8993068334655447 ) ) ;
#211148=VECTOR ( 'NONE', #20028, 1000.000000000000000 ) ;
#211167=CARTESIAN_POINT ( 'NONE',  ( -16.93521499325732194, 66.00521388020901270, -182.6159989434308955 ) ) ;
#211348=AXIS2_PLACEMENT_3D ( 'NONE', #214048, #152825, #172401 ) ;
#211424=CARTESIAN_POINT ( 'NONE',  ( -16.86445178670597045, 66.03778837089667775, -190.9138849226415005 ) ) ;
#211940=FACE_OUTER_BOUND ( 'NONE', #142665, .T. ) ;
#212001=EDGE_CURVE ( 'NONE', #243580, #95790, #82225, .T. ) ;
#212052=ORIENTED_EDGE ( 'NONE', *, *, #152556, .T. ) ;
#212097=ORIENTED_EDGE ( 'NONE', *, *, #10899, .T. ) ;
#212420=ORIENTED_EDGE ( 'NONE', *, *, #242240, .F. ) ;
#212539=CARTESIAN_POINT ( 'NONE',  ( -16.79140778683511215, 66.05505840115797866, -182.6933702507536452 ) ) ;
#212619=CARTESIAN_POINT ( 'NONE',  ( -16.87683809663752399, 54.76195096157953657, -190.8731074845245246 ) ) ;
#213127=PLANE ( 'NONE',  #29678 ) ;
#213152=CARTESIAN_POINT ( 'NONE',  ( 21.72449340488910252, 65.71604372252150483, -194.2731074845244166 ) ) ;
#213168=CARTESIAN_POINT ( 'NONE',  ( -16.87036670365548474, 65.91505003675726471, -182.5731074845244279 ) ) ;
#213183=DIRECTION ( 'NONE',  ( 0.7071067811865456854, 0.7071067811865493491, 4.937700262164544098E-15 ) ) ;
#213235=AXIS2_PLACEMENT_3D ( 'NONE', #76871, #156462, #37780 ) ;
#213303=VERTEX_POINT ( 'NONE', #105883 ) ;
#213476=VECTOR ( 'NONE', #46407, 1000.000000000000000 ) ;
#213801=CARTESIAN_POINT ( 'NONE',  ( -16.85312964099708566, 66.08639531794483446, -182.9202917780939970 ) ) ;
#213905=CARTESIAN_POINT ( 'NONE',  ( -18.34374000495060386, 64.52683809665015247, -194.2731074845244450 ) ) ;
#213915=EDGE_CURVE ( 'NONE', #24375, #178700, #102364, .T. ) ;
#214048=CARTESIAN_POINT ( 'NONE',  ( 20.73486653747088937, 68.25000000001259082, -194.2731074845244166 ) ) ;
#214169=EDGE_CURVE ( 'NONE', #219313, #70737, #16172, .T. ) ;
#214255=CARTESIAN_POINT ( 'NONE',  ( -16.89060415895971090, 66.04877923721039679, -190.8771872602539474 ) ) ;
#214438=EDGE_CURVE ( 'NONE', #199921, #194460, #206346, .T. ) ;
#214445=DIRECTION ( 'NONE',  ( 0.000000000000000000, 0.9553114395363127009, 0.2956011730204364252 ) ) ;
#214522=EDGE_CURVE ( 'NONE', #250290, #74558, #109791, .T. ) ;
#214827=CARTESIAN_POINT ( 'NONE',  ( -16.92507428761700439, 66.05000000001261640, -190.8097100249028699 ) ) ;
#214896=EDGE_CURVE ( 'NONE', #180338, #113296, #177670, .T. ) ;
#215031=EDGE_CURVE ( 'NONE', #228950, #232210, #52072, .T. ) ;
#215431=VECTOR ( 'NONE', #258033, 1000.000000000000000 ) ;
#215482=CARTESIAN_POINT ( 'NONE',  ( 18.39999999999999503, 64.52683809665003878, -179.2731074845244450 ) ) ;
#215494=ORIENTED_EDGE ( 'NONE', *, *, #188015, .F. ) ;
#215952=AXIS2_PLACEMENT_3D ( 'NONE', #186545, #209966, #7915 ) ;
#216013=LINE ( 'NONE', #20416, #243283 ) ;
#216078=VECTOR ( 'NONE', #6633, 1000.000000000000000 ) ;
#216368=ORIENTED_EDGE ( 'NONE', *, *, #72904, .T. ) ;
#216447=DIRECTION ( 'NONE',  ( 1.000000000000000000, -1.186688945009010077E-16, -8.286604613020808509E-31 ) ) ;
#216506=CARTESIAN_POINT ( 'NONE',  ( -20.65000000000000568, 70.35000000001261355, -190.8731074845244109 ) ) ;
#216617=VERTEX_POINT ( 'NONE', #39278 ) ;
#216792=CARTESIAN_POINT ( 'NONE',  ( -17.11825945287481332, 65.95000000001255103, -182.7731074845244450 ) ) ;
#216883=ORIENTED_EDGE ( 'NONE', *, *, #256768, .F. ) ;
#216899=DIRECTION ( 'NONE',  ( -1.020425574104004196E-15, 6.982962677686266711E-15, -1.000000000000000000 ) ) ;
#217002=EDGE_LOOP ( 'NONE', ( #241597, #51220, #71715, #59623 ) ) ;
#217120=FACE_OUTER_BOUND ( 'NONE', #142570, .T. ) ;
#217154=VECTOR ( 'NONE', #5610, 1000.000000000000000 ) ;
#217334=DIRECTION ( 'NONE',  ( 1.000000000000000000, -0.000000000000000000, 0.000000000000000000 ) ) ;
#217346=CARTESIAN_POINT ( 'NONE',  ( 20.99999999999999645, 66.25000000001261924, -190.8731074845244393 ) ) ;
#217524=CARTESIAN_POINT ( 'NONE',  ( 13.99999999999999822, 66.15000000001258229, -186.7731074845244450 ) ) ;
#217870=FACE_OUTER_BOUND ( 'NONE', #219365, .T. ) ;
#217979=CARTESIAN_POINT ( 'NONE',  ( -21.65000000000000213, 66.05000000001255955, -182.7731074845244450 ) ) ;
#217982=LINE ( 'NONE', #160636, #115328 ) ;
#218060=DIRECTION ( 'NONE',  ( -0.7071067811865487940, -0.7071067811865463515, -4.937700262164522799E-15 ) ) ;
#218067=ORIENTED_EDGE ( 'NONE', *, *, #29260, .F. ) ;
#218102=( BOUNDED_CURVE ( )  B_SPLINE_CURVE ( 3, ( #44963, #82755, #161065, #123210 ),
 .UNSPECIFIED., .F., .F. ) 
 B_SPLINE_CURVE_WITH_KNOTS ( ( 4, 4 ),
 ( 0.3000847527772370071, 0.5497968875596834781 ),
 .UNSPECIFIED. ) 
 CURVE ( )  GEOMETRIC_REPRESENTATION_ITEM ( )  RATIONAL_B_SPLINE_CURVE ( ( 1.000000000000000000, 0.9948104011409417691, 0.9948104011409417691, 1.000000000000000000 ) ) 
 REPRESENTATION_ITEM ( '' )  );
#218122=CARTESIAN_POINT ( 'NONE',  ( -18.40000000000000568, 64.58541674041275371, -182.6731074845244223 ) ) ;
#218144=CARTESIAN_POINT ( 'NONE',  ( -16.93658211146646408, 66.00589133767141448, -190.9274025544800963 ) ) ;
#218318=LINE ( 'NONE', #200071, #161710 ) ;
#218360=CARTESIAN_POINT ( 'NONE',  ( -18.40000000000000213, 64.52683809665056458, -179.3229367329901436 ) ) ;
#218487=STYLED_ITEM ( 'NONE', ( #43367 ), #198047 ) ;
#218604=DIRECTION ( 'NONE',  ( 0.000000000000000000, 1.000000000000000000, 6.982962677686266711E-15 ) ) ;
#218810=CYLINDRICAL_SURFACE ( 'NONE', #97435, 1.749999999999998002 ) ;
#219166=EDGE_CURVE ( 'NONE', #237439, #169837, #72073, .T. ) ;
#219192=CARTESIAN_POINT ( 'NONE',  ( -18.40000000000000213, 70.35000000001261355, -190.8731074845244109 ) ) ;
#219313=VERTEX_POINT ( 'NONE', #245117 ) ;
#219337=CARTESIAN_POINT ( 'NONE',  ( -15.06720934482786234, 66.58230930894947619, -185.3815067877598324 ) ) ;
#219365=EDGE_LOOP ( 'NONE', ( #79060, #956, #89626, #77887 ) ) ;
#219784=DIRECTION ( 'NONE',  ( -1.000000000000000000, 4.625929269271478222E-14, 0.000000000000000000 ) ) ;
#220421=ADVANCED_FACE ( 'NONE', ( #147493 ), #27584, .F. ) ;
#220672=CARTESIAN_POINT ( 'NONE',  ( 15.74999999999999645, 66.65000000001258229, -186.7731074845244166 ) ) ;
#220764=ORIENTED_EDGE ( 'NONE', *, *, #172367, .T. ) ;
#220770=ORIENTED_EDGE ( 'NONE', *, *, #7623, .T. ) ;
#220845=CARTESIAN_POINT ( 'NONE',  ( 23.24999999999999645, 67.17743825834619997, -190.8731074845244109 ) ) ;
#220907=CARTESIAN_POINT ( 'NONE',  ( -16.27683809663750480, 66.65000000001263913, -194.2731074845244166 ) ) ;
#220924=AXIS2_PLACEMENT_3D ( 'NONE', #154859, #75325, #153602 ) ;
#220989=DIRECTION ( 'NONE',  ( -0.000000000000000000, -6.982962677686266711E-15, 1.000000000000000000 ) ) ;
#221056=CARTESIAN_POINT ( 'NONE',  ( -13.12432614554023935, 66.56923500459026855, -188.2925700897739887 ) ) ;
#221133=ORIENTED_EDGE ( 'NONE', *, *, #138324, .F. ) ;
#221201=DIRECTION ( 'NONE',  ( -1.000000000000000000, 0.000000000000000000, 0.000000000000000000 ) ) ;
#221545=DIRECTION ( 'NONE',  ( -1.000000000000000000, 0.000000000000000000, 0.000000000000000000 ) ) ;
#221600=CARTESIAN_POINT ( 'NONE',  ( -16.97683809663754317, 66.05000000001258798, -183.2946366524139137 ) ) ;
#221649=CARTESIAN_POINT ( 'NONE',  ( -16.87786941232800686, 66.04184528586756642, -182.6459216847304390 ) ) ;
#221669=CARTESIAN_POINT ( 'NONE',  ( 13.99999999999999822, 66.15000000001258229, -186.7731074845244450 ) ) ;
#221782=VECTOR ( 'NONE', #232790, 1000.000000000000000 ) ;
#221845=CARTESIAN_POINT ( 'NONE',  ( 20.05000000000002913, 68.75000000001257661, -190.8731074845244109 ) ) ;
#221894=VERTEX_POINT ( 'NONE', #27320 ) ;
#222318=CARTESIAN_POINT ( 'NONE',  ( -13.43673303185030221, 66.55335100938371795, -188.4339441886012025 ) ) ;
#222510=CARTESIAN_POINT ( 'NONE',  ( -16.27683809663751191, 66.65000000001262492, -190.9731074845244336 ) ) ;
#223074=DIRECTION ( 'NONE',  ( -1.000000000000000000, 0.000000000000000000, -0.000000000000000000 ) ) ;
#223186=CARTESIAN_POINT ( 'NONE',  ( -14.56336952470178758, 66.55335465531733519, -185.1123010284241843 ) ) ;
#223341=CARTESIAN_POINT ( 'NONE',  ( -18.34374000495059676, 64.52683809665003878, -179.2731074845244450 ) ) ;
#223463=CARTESIAN_POINT ( 'NONE',  ( -16.87242674293849021, 66.05000000001255955, -182.6720172381520797 ) ) ;
#223626=CIRCLE ( 'NONE', #207099, 14.20833333333333748 ) ;
#223740=LINE ( 'NONE', #122100, #34507 ) ;
#223783=DIRECTION ( 'NONE',  ( 0.000000000000000000, 6.982962677686266711E-15, -1.000000000000000000 ) ) ;
#223787=DIRECTION ( 'NONE',  ( 0.000000000000000000, 6.982962677686266711E-15, -1.000000000000000000 ) ) ;
#224245=DIRECTION ( 'NONE',  ( 1.000000000000000000, 0.000000000000000000, 0.000000000000000000 ) ) ;
#224285=CARTESIAN_POINT ( 'NONE',  ( 12.68104795156995301, 66.60346600605868161, -185.6171677053511928 ) ) ;
#224737=ORIENTED_EDGE ( 'NONE', *, *, #57799, .T. ) ;
#224795=ADVANCED_FACE ( 'NONE', ( #102740 ), #84438, .F. ) ;
#224846=CARTESIAN_POINT ( 'NONE',  ( -16.93710578446435377, 66.05000000001255955, -182.9419114683242640 ) ) ;
#224880=EDGE_LOOP ( 'NONE', ( #29997, #212097, #238078, #241860 ) ) ;
#224901=CARTESIAN_POINT ( 'NONE',  ( -13.88555196119804691, 66.54256847116366202, -188.5231905466247611 ) ) ;
#224990=DIRECTION ( 'NONE',  ( 1.000000000000000000, 0.000000000000000000, 0.000000000000000000 ) ) ;
#225305=FACE_OUTER_BOUND ( 'NONE', #238333, .T. ) ;
#225431=AXIS2_PLACEMENT_3D ( 'NONE', #213168, #55342, #214445 ) ;
#225456=CARTESIAN_POINT ( 'NONE',  ( -16.92989507731676468, 66.05000000001254534, -182.9056085539142487 ) ) ;
#225544=CARTESIAN_POINT ( 'NONE',  ( 12.60873083341399514, 66.61042836546617707, -185.7054667721552903 ) ) ;
#225710=B_SPLINE_CURVE_WITH_KNOTS ( 'NONE', 3,
 ( #248594, #69981, #189908, #109072, #34707, #114219, #167805, #13841, #11274, #251139 ),
 .UNSPECIFIED., .F., .F.,
 ( 4, 3, 3, 4 ),
 ( -2.000561356218653466E-06, 0.000000000000000000, 1.787822682428266431E-05, 4.206475347089651067E-05 ),
 .UNSPECIFIED. ) ;
#225854=CARTESIAN_POINT ( 'NONE',  ( 18.39999999999997371, 64.25000000001264766, -194.2731074845244450 ) ) ;
#225885=CARTESIAN_POINT ( 'NONE',  ( -17.11825945287481332, 65.95000000001255103, -182.6731074845244223 ) ) ;
#225933=CARTESIAN_POINT ( 'NONE',  ( 18.54999999999999716, 66.05000000001254534, -182.6731074845243654 ) ) ;
#226393=EDGE_CURVE ( 'NONE', #54689, #76475, #247136, .T. ) ;
#226424=CARTESIAN_POINT ( 'NONE',  ( -16.77828822508139694, 66.05377062509185748, -190.8604792331504711 ) ) ;
#226458=EDGE_CURVE ( 'NONE', #194584, #180208, #242010, .T. ) ;
#226560=ADVANCED_FACE ( 'NONE', ( #34544 ), #252268, .F. ) ;
#226610=EDGE_LOOP ( 'NONE', ( #172375, #134282, #181975, #13699, #27742, #157427 ) ) ;
#226705=CARTESIAN_POINT ( 'NONE',  ( 20.73486653747088582, 68.75000000001257661, -190.8731074845244109 ) ) ;
#227309=VECTOR ( 'NONE', #49752, 1000.000000000000000 ) ;
#227419=CARTESIAN_POINT ( 'NONE',  ( -16.83558968593874994, 66.05000000001255955, -182.6854126721411262 ) ) ;
#227641=DIRECTION ( 'NONE',  ( -0.8049926720990042694, 0.5932847527679310229, 4.142885285818786163E-15 ) ) ;
#227766=EDGE_CURVE ( 'NONE', #178700, #110389, #63746, .T. ) ;
#228088=ADVANCED_FACE ( 'NONE', ( #181656 ), #199944, .F. ) ;
#228186=VECTOR ( 'NONE', #91960, 1000.000000000000000 ) ;
#228216=CARTESIAN_POINT ( 'NONE',  ( 12.25000000000000000, 66.65000000001258229, -186.7731074845244166 ) ) ;
#228410=B_SPLINE_CURVE_WITH_KNOTS ( 'NONE', 3,
 ( #132934, #192901, #114638, #50788 ),
 .UNSPECIFIED., .F., .F.,
 ( 4, 4 ),
 ( 0.000000000000000000, 7.713889350930586977E-05 ),
 .UNSPECIFIED. ) ;
#228648=ORIENTED_EDGE ( 'NONE', *, *, #99944, .F. ) ;
#228888=( NAMED_UNIT ( * ) PLANE_ANGLE_UNIT ( ) SI_UNIT ( $, .RADIAN. ) );
#228950=VERTEX_POINT ( 'NONE', #90574 ) ;
#229031=CARTESIAN_POINT ( 'NONE',  ( -16.78569801330234057, 66.05206626689910365, -190.8661945791769199 ) ) ;
#229410=ORIENTED_EDGE ( 'NONE', *, *, #72956, .T. ) ;
#229451=CARTESIAN_POINT ( 'NONE',  ( -16.93344882324368683, 66.00341123272467314, -182.6100817897194872 ) ) ;
#229465=VECTOR ( 'NONE', #121632, 1000.000000000000000 ) ;
#229621=ORIENTED_EDGE ( 'NONE', *, *, #219166, .T. ) ;
#229757=CARTESIAN_POINT ( 'NONE',  ( -16.77683809663752257, 66.05416425680839154, -182.6870565036286393 ) ) ;
#229920=EDGE_CURVE ( 'NONE', #54771, #235005, #96383, .T. ) ;
#230072=B_SPLINE_CURVE_WITH_KNOTS ( 'NONE', 3,
 ( #42226, #241702, #20096, #181732, #237847, #99589, #57906, #239135, #158350, #159606 ),
 .UNSPECIFIED., .F., .F.,
 ( 4, 3, 3, 4 ),
 ( 1.883833020489685736E-15, 3.877043166999269576E-05, 7.336897548475664402E-05, 7.659383120240691504E-05 ),
 .UNSPECIFIED. ) ;
#230213=CARTESIAN_POINT ( 'NONE',  ( -18.44085059012131822, 64.48598750652882927, -194.2634128036459913 ) ) ;
#230479=CARTESIAN_POINT ( 'NONE',  ( -16.85939591225058720, 66.09477352162475938, -190.5630392380553815 ) ) ;
#230685=VECTOR ( 'NONE', #181008, 1000.000000000000000 ) ;
#230780=ORIENTED_EDGE ( 'NONE', *, *, #158878, .F. ) ;
#230937=EDGE_CURVE ( 'NONE', #70737, #237439, #117531, .T. ) ;
#231027=ORIENTED_EDGE ( 'NONE', *, *, #163950, .F. ) ;
#231112=VECTOR ( 'NONE', #38902, 1000.000000000000000 ) ;
#231136=CARTESIAN_POINT ( 'NONE',  ( -16.94107738177414291, 65.98576071487592287, -182.5731074845244279 ) ) ;
#231290=CIRCLE ( 'NONE', #35495, 1.749999999999998002 ) ;
#231413=( BOUNDED_CURVE ( )  B_SPLINE_CURVE ( 3, ( #26449, #85087, #150253, #225885 ),
 .UNSPECIFIED., .F., .F. ) 
 B_SPLINE_CURVE_WITH_KNOTS ( ( 4, 4 ),
 ( 3.752122642744585068, 4.712388980384675463 ),
 .UNSPECIFIED. ) 
 CURVE ( )  GEOMETRIC_REPRESENTATION_ITEM ( )  RATIONAL_B_SPLINE_CURVE ( ( 1.000000000000000000, 0.9246222802177217481, 0.9246222802177217481, 1.000000000000000000 ) ) 
 REPRESENTATION_ITEM ( '' )  );
#231600=CARTESIAN_POINT ( 'NONE',  ( -16.80438519320023616, 66.05022090354425757, -190.8723692036031423 ) ) ;
#232164=CARTESIAN_POINT ( 'NONE',  ( -16.80070461187793995, 66.05000000001261640, -190.8761436553694182 ) ) ;
#232210=VERTEX_POINT ( 'NONE', #146120 ) ;
#232392=EDGE_CURVE ( 'NONE', #13472, #71999, #242168, .T. ) ;
#232539=ORIENTED_EDGE ( 'NONE', *, *, #68976, .T. ) ;
#232790=DIRECTION ( 'NONE',  ( -0.7071067811865463515, -0.7071067811865487940, -4.937700262164540154E-15 ) ) ;
#233067=CARTESIAN_POINT ( 'NONE',  ( -16.87683809663753465, 66.13508622147418237, -190.2473918488859397 ) ) ;
#233114=LINE ( 'NONE', #76574, #196015 ) ;
#233160=CARTESIAN_POINT ( 'NONE',  ( -18.34804628011471195, 64.52683809665025194, -194.2731074845244450 ) ) ;
#233208=CARTESIAN_POINT ( 'NONE',  ( 18.54999999999999716, 67.25000000001259082, -194.2731074845244166 ) ) ;
#233292=DIRECTION ( 'NONE',  ( -1.000000000000000000, 0.000000000000000000, 0.000000000000000000 ) ) ;
#233392=FACE_BOUND ( 'NONE', #48918, .T. ) ;
#233422=DIRECTION ( 'NONE',  ( 1.000000000000000000, 0.000000000000000000, 0.000000000000000000 ) ) ;
#233447=ORIENTED_EDGE ( 'NONE', *, *, #60027, .F. ) ;
#233458=SHAPE_DEFINITION_REPRESENTATION ( #53639, #170171 ) ;
#233523=DIRECTION ( 'NONE',  ( -1.000000000000000000, 0.000000000000000000, -0.000000000000000000 ) ) ;
#233820=CARTESIAN_POINT ( 'NONE',  ( -16.87331047859651179, 66.05000000001261640, -190.8731074845244393 ) ) ;
#233959=ORIENTED_EDGE ( 'NONE', *, *, #158878, .T. ) ;
#234259=CARTESIAN_POINT ( 'NONE',  ( -18.40000000000000213, 64.51332499825484490, -179.2731074845244450 ) ) ;
#234359=DIRECTION ( 'NONE',  ( 1.652117596168391700E-15, -1.000000000000000000, -6.982962677686266711E-15 ) ) ;
#234450=DIRECTION ( 'NONE',  ( 0.000000000000000000, -6.982962677686266711E-15, 1.000000000000000000 ) ) ;
#234474=ADVANCED_FACE ( 'NONE', ( #7012 ), #1854, .F. ) ;
#234743=ORIENTED_EDGE ( 'NONE', *, *, #236978, .T. ) ;
#235005=VERTEX_POINT ( 'NONE', #125735 ) ;
#235023=CARTESIAN_POINT ( 'NONE',  ( -16.81744102076749314, 66.05000000001261640, -190.8731074845244393 ) ) ;
#235104=CARTESIAN_POINT ( 'NONE',  ( 12.84233041328155878, 66.58946139148369525, -188.0904194873834854 ) ) ;
#235170=CARTESIAN_POINT ( 'NONE',  ( -16.94107738177415712, 65.98576071487597972, -190.9731074845244336 ) ) ;
#235208=CARTESIAN_POINT ( 'NONE',  ( 18.39999999999999503, 64.25000000001256240, -182.6731074845244507 ) ) ;
#235290=B_SPLINE_CURVE_WITH_KNOTS ( 'NONE', 3,
 ( #60227, #58919, #240171, #236301, #156802, #117644, #57650, #118944, #158103, #99337 ),
 .UNSPECIFIED., .F., .F.,
 ( 4, 3, 3, 4 ),
 ( 0.000000000000000000, 1.004626015991452777E-05, 1.831183478182391193E-05, 2.062343583995917743E-05 ),
 .UNSPECIFIED. ) ;
#235555=ORIENTED_EDGE ( 'NONE', *, *, #137104, .T. ) ;
#235687=CARTESIAN_POINT ( 'NONE',  ( -18.37160782347004329, 64.52438358521023076, -194.2731074845244450 ) ) ;
#235738=CARTESIAN_POINT ( 'NONE',  ( 18.39999999999999503, 70.35000000001261355, -190.8731074845244109 ) ) ;
#235830=ORIENTED_EDGE ( 'NONE', *, *, #227766, .F. ) ;
#235932=LINE ( 'NONE', #241100, #156019 ) ;
#235987=CARTESIAN_POINT ( 'NONE',  ( -16.77308656112215246, 66.05000000001258798, -190.8729142928220881 ) ) ;
#236066=CARTESIAN_POINT ( 'NONE',  ( 23.24999999999999645, 64.25000000001264766, -194.2731074845244450 ) ) ;
#236301=CARTESIAN_POINT ( 'NONE',  ( -16.88328101497759448, 66.04964716579368655, -182.6719279695951457 ) ) ;
#236369=VECTOR ( 'NONE', #216899, 1000.000000000000000 ) ;
#236375=CARTESIAN_POINT ( 'NONE',  ( 15.39793903038208001, 66.61031399435691469, -187.8502639781730750 ) ) ;
#236479=LINE ( 'NONE', #235208, #211148 ) ;
#236501=EDGE_CURVE ( 'NONE', #38279, #197652, #97538, .T. ) ;
#236609=AXIS2_PLACEMENT_3D ( 'NONE', #163454, #201287, #87747 ) ;
#236778=CARTESIAN_POINT ( 'NONE',  ( 20.99999999999999645, 66.25000000001261924, -190.8731074845244393 ) ) ;
#236978=EDGE_CURVE ( 'NONE', #104788, #235005, #194153, .T. ) ;
#237099=EDGE_LOOP ( 'NONE', ( #65815, #88248, #120322, #251623, #161911, #253103 ) ) ;
#237117=PLANE ( 'NONE',  #151398 ) ;
#237439=VERTEX_POINT ( 'NONE', #209527 ) ;
#237459=DIRECTION ( 'NONE',  ( 0.000000000000000000, -1.000000000000000000, -6.982962677686266711E-15 ) ) ;
#237643=EDGE_CURVE ( 'NONE', #86769, #216617, #173189, .T. ) ;
#237654=CARTESIAN_POINT ( 'NONE',  ( 16.27683809663750125, 66.65000000001263913, -194.2731074845244166 ) ) ;
#237714=CARTESIAN_POINT ( 'NONE',  ( -18.40000000000000568, 64.52683809665006720, -182.6316861282871287 ) ) ;
#237827=ADVANCED_BREP_SHAPE_REPRESENTATION ( '', ( #198047, #2425 ), #185768 ) ;
#237847=CARTESIAN_POINT ( 'NONE',  ( -16.92925196614875105, 66.02766820360247380, -190.9063626368076427 ) ) ;
#238049=CARTESIAN_POINT ( 'NONE',  ( -16.92989143108097849, 66.05000000001261640, -190.6406236097677720 ) ) ;
#238078=ORIENTED_EDGE ( 'NONE', *, *, #188048, .T. ) ;
#238245=ADVANCED_FACE ( 'NONE', ( #143933 ), #155981, .T. ) ;
#238254=CARTESIAN_POINT ( 'NONE',  ( -18.40000000000000213, 64.51332499825495859, -194.2731074845244450 ) ) ;
#238265=CARTESIAN_POINT ( 'NONE',  ( 20.73486653747088582, 68.75000000001259082, -194.2731074845244166 ) ) ;
#238278=ADVANCED_FACE ( 'NONE', ( #92948 ), #8299, .F. ) ;
#238305=FACE_OUTER_BOUND ( 'NONE', #89094, .T. ) ;
#238333=EDGE_LOOP ( 'NONE', ( #110706, #90239, #76697, #235830 ) ) ;
#238438=EDGE_CURVE ( 'NONE', #239104, #252537, #138472, .T. ) ;
#238529=AXIS2_PLACEMENT_3D ( 'NONE', #247206, #227641, #192379 ) ;
#238651=FACE_OUTER_BOUND ( 'NONE', #150981, .T. ) ;
#238918=CARTESIAN_POINT ( 'NONE',  ( -15.51798037960204546, 66.62334006147904120, -185.8949149363071456 ) ) ;
#238959=CARTESIAN_POINT ( 'NONE',  ( 12.25000000000000000, 66.65000000001258229, -186.7731074845244166 ) ) ;
#238961=EDGE_CURVE ( 'NONE', #104084, #256760, #42952, .T. ) ;
#238995=CARTESIAN_POINT ( 'NONE',  ( 22.88900146558018989, 67.29609520889979990, -194.2731074845244166 ) ) ;
#239104=VERTEX_POINT ( 'NONE', #226705 ) ;
#239135=CARTESIAN_POINT ( 'NONE',  ( -16.94333152886235894, 66.00965798856212530, -190.9151390155788306 ) ) ;
#239228=CARTESIAN_POINT ( 'NONE',  ( -12.25000000000000178, 66.65000000001258229, -186.7731074845244166 ) ) ;
#239288=PLANE ( 'NONE',  #125366 ) ;
#239299=CARTESIAN_POINT ( 'NONE',  ( -16.94107738177414291, 65.98576071487592287, -182.5731074845244279 ) ) ;
#239368=CARTESIAN_POINT ( 'NONE',  ( -16.94107738177413225, 65.98576071487593708, -182.5731074845244564 ) ) ;
#239415=ORIENTED_EDGE ( 'NONE', *, *, #203386, .T. ) ;
#240012=CARTESIAN_POINT ( 'NONE',  ( 14.88075390448864077, 66.56831044948847875, -185.2438174522883685 ) ) ;
#240171=CARTESIAN_POINT ( 'NONE',  ( -16.88005004766534967, 66.04989949669150917, -182.6727713725756530 ) ) ;
#240210=CARTESIAN_POINT ( 'NONE',  ( -15.66061380678751647, 66.63927620602653690, -186.2091802899176969 ) ) ;
#240461=LINE ( 'NONE', #60522, #12283 ) ;
#240465=ORIENTED_EDGE ( 'NONE', *, *, #11161, .T. ) ;
#240474=CARTESIAN_POINT ( 'NONE',  ( -17.11825945287481687, 66.05000000001255955, -182.7731074845244450 ) ) ;
#240569=LINE ( 'NONE', #61936, #121117 ) ;
#240976=VECTOR ( 'NONE', #199786, 1000.000000000000000 ) ;
#241067=EDGE_CURVE ( 'NONE', #74558, #142715, #65785, .T. ) ;
#241100=CARTESIAN_POINT ( 'NONE',  ( -16.87683809663752399, 66.05000000001261640, -190.8731074845244393 ) ) ;
#241155=CYLINDRICAL_SURFACE ( 'NONE', #29549, 0.9000000000000014655 ) ;
#241202=CARTESIAN_POINT ( 'NONE',  ( -17.11825945287482753, 65.95000000001262208, -190.8731074845244109 ) ) ;
#241210=CARTESIAN_POINT ( 'NONE',  ( -16.94226253665224391, 66.05000000001254534, -182.9698420801401539 ) ) ;
#241276=FACE_OUTER_BOUND ( 'NONE', #79579, .T. ) ;
#241305=CARTESIAN_POINT ( 'NONE',  ( 13.54577453029516398, 66.54939790392401733, -185.0792115214277658 ) ) ;
#241402=EDGE_LOOP ( 'NONE', ( #60074, #53088, #83745 ) ) ;
#241597=ORIENTED_EDGE ( 'NONE', *, *, #256856, .F. ) ;
#241702=CARTESIAN_POINT ( 'NONE',  ( -16.90257928357874206, 66.04589317890723521, -190.8868220544107430 ) ) ;
#241716=ORIENTED_EDGE ( 'NONE', *, *, #145660, .F. ) ;
#241740=EDGE_LOOP ( 'NONE', ( #42047, #122316, #199404, #65597 ) ) ;
#241845=CARTESIAN_POINT ( 'NONE',  ( -16.82542659449977762, 66.06550010858508415, -182.7677430845504318 ) ) ;
#241860=ORIENTED_EDGE ( 'NONE', *, *, #236501, .T. ) ;
#241873=ORIENTED_EDGE ( 'NONE', *, *, #7003, .F. ) ;
#241897=CARTESIAN_POINT ( 'NONE',  ( -16.94225986326249611, 66.05000000001261640, -190.5763881089164897 ) ) ;
#241995=ORIENTED_EDGE ( 'NONE', *, *, #189710, .F. ) ;
#242010=LINE ( 'NONE', #43821, #63919 ) ;
#242046=B_SPLINE_CURVE_WITH_KNOTS ( 'NONE', 3,
 ( #162399, #24173, #247040, #7146, #187107, #8454, #26750, #164950, #106237, #167547, #82804, #245777, #103664 ),
 .UNSPECIFIED., .F., .F.,
 ( 4, 3, 3, 3, 4 ),
 ( -3.224855718275878119E-06, -4.235164736271501695E-22, 6.199515528669195097E-06, 4.034952380127538728E-05, 7.452715123699865944E-05 ),
 .UNSPECIFIED. ) ;
#242148=EDGE_CURVE ( 'NONE', #196258, #108824, #43283, .T. ) ;
#242168=B_SPLINE_CURVE_WITH_KNOTS ( 'NONE', 3,
 ( #192966, #151278, #134246, #52143, #213801, #131698, #15637, #191707, #13061, #53448, #132998, #212539, #33937, #113420 ),
 .UNSPECIFIED., .F., .F.,
 ( 4, 2, 2, 2, 2, 2, 4 ),
 ( 0.000000000000000000, 0.0003823333598417659224, 0.0005735000397626485854, 0.0006690833797230926003, 0.0007168750497033104336, 0.0007407708846934199466, 0.0007646667196835293511 ),
 .UNSPECIFIED. ) ;
#242240=EDGE_CURVE ( 'NONE', #135464, #2493, #30153, .T. ) ;
#242358=CARTESIAN_POINT ( 'NONE',  ( -21.65000000000000213, 68.75000000001263345, -194.2731074845244166 ) ) ;
#242462=CARTESIAN_POINT ( 'NONE',  ( -16.84419801905646352, 66.05000000001257376, -182.6925973307465085 ) ) ;
#242745=DIRECTION ( 'NONE',  ( 1.186688945009009831E-16, 1.000000000000000000, 6.982962677686266711E-15 ) ) ;
#242787=FACE_OUTER_BOUND ( 'NONE', #140187, .T. ) ;
#242841=DIRECTION ( 'NONE',  ( -1.000000000000000000, 0.000000000000000000, 0.000000000000000000 ) ) ;
#242970=VERTEX_POINT ( 'NONE', #60920 ) ;
#243127=AXIS2_PLACEMENT_3D ( 'NONE', #75503, #16806, #233292 ) ;
#243131=CARTESIAN_POINT ( 'NONE',  ( -16.77180007708462028, 66.05000000001255955, -182.6587216034792505 ) ) ;
#243262=EDGE_LOOP ( 'NONE', ( #87718, #78784, #244120, #125734, #200333 ) ) ;
#243283=VECTOR ( 'NONE', #80335, 1000.000000000000000 ) ;
#243308=DIRECTION ( 'NONE',  ( -1.000000000000000000, 7.492892343619937423E-30, -1.073024830501117725E-15 ) ) ;
#243353=ORIENTED_EDGE ( 'NONE', *, *, #124260, .F. ) ;
#243368=ADVANCED_FACE ( 'NONE', ( #142718 ), #21521, .T. ) ;
#243390=LINE ( 'NONE', #200422, #69313 ) ;
#243513=ORIENTED_EDGE ( 'NONE', *, *, #7513, .F. ) ;
#243530=LINE ( 'NONE', #100140, #230685 ) ;
#243564=ORIENTED_EDGE ( 'NONE', *, *, #103050, .T. ) ;
#243580=VERTEX_POINT ( 'NONE', #216506 ) ;
#243725=CARTESIAN_POINT ( 'NONE',  ( -18.40000000000000213, 70.35000000001254250, -179.2731074845243882 ) ) ;
#243868=ORIENTED_EDGE ( 'NONE', *, *, #68976, .F. ) ;
#244035=CARTESIAN_POINT ( 'NONE',  ( -13.11924609551134857, 66.56831044948847875, -185.2438174522883685 ) ) ;
#244073=DIRECTION ( 'NONE',  ( 0.000000000000000000, 0.000000000000000000, -1.000000000000000000 ) ) ;
#244120=ORIENTED_EDGE ( 'NONE', *, *, #161502, .F. ) ;
#244311=CARTESIAN_POINT ( 'NONE',  ( -16.95709691156737620, 66.05000000001255955, -182.6831650470390969 ) ) ;
#244517=EDGE_CURVE ( 'NONE', #154893, #81857, #218102, .T. ) ;
#244888=CYLINDRICAL_SURFACE ( 'NONE', #247273, 1.749999999999999778 ) ;
#245117=CARTESIAN_POINT ( 'NONE',  ( 18.39999999999999503, 64.25000000001261924, -190.8731074845244393 ) ) ;
#245249=FACE_OUTER_BOUND ( 'NONE', #22564, .T. ) ;
#245263=LINE ( 'NONE', #48332, #216078 ) ;
#245413=EDGE_CURVE ( 'NONE', #208807, #147103, #152940, .T. ) ;
#245777=CARTESIAN_POINT ( 'NONE',  ( -16.90128866880176872, 66.04620422280959247, -182.6604313011357874 ) ) ;
#245885=B_SPLINE_CURVE_WITH_KNOTS ( 'NONE', 3,
 ( #183789, #242462, #101644, #161680, #67687, #225456, #241210, #200783, #221600, #63843 ),
 .UNSPECIFIED., .F., .F.,
 ( 4, 2, 2, 2, 4 ),
 ( 5.247129907028296623E-16, 9.930191194501768691E-05, 0.0001986038238895106471, 0.0003972076477784965945, 0.0007944152955563852769 ),
 .UNSPECIFIED. ) ;
#245942=PLANE ( 'NONE',  #238529 ) ;
#246356=AXIS2_PLACEMENT_3D ( 'NONE', #144243, #25612, #223787 ) ;
#246791=ADVANCED_FACE ( 'NONE', ( #211940 ), #170280, .F. ) ;
#246980=CARTESIAN_POINT ( 'NONE',  ( -16.88783316861802319, 66.05000000001255955, -182.7753715265037044 ) ) ;
#247012=CARTESIAN_POINT ( 'NONE',  ( -16.88495309932524080, 66.04537294153973903, -190.8885588107125386 ) ) ;
#247040=CARTESIAN_POINT ( 'NONE',  ( -16.94333152882356330, 66.00965798855487776, -182.6310759534229646 ) ) ;
#247136=LINE ( 'NONE', #47643, #255389 ) ;
#247206=CARTESIAN_POINT ( 'NONE',  ( 20.27550659511088682, 66.78395627750377628, -194.2731074845244166 ) ) ;
#247223=CIRCLE ( 'NONE', #151588, 0.1000000000000028644 ) ;
#247273=AXIS2_PLACEMENT_3D ( 'NONE', #127520, #106641, #207058 ) ;
#247305=VECTOR ( 'NONE', #170930, 1000.000000000000000 ) ;
#247430=ADVANCED_FACE ( 'NONE', ( #82025 ), #241155, .F. ) ;
#247872=DIRECTION ( 'NONE',  ( 1.000000000000000000, 0.000000000000000000, 0.000000000000000000 ) ) ;
#247971=FACE_OUTER_BOUND ( 'NONE', #86109, .T. ) ;
#247997=ORIENTED_EDGE ( 'NONE', *, *, #252223, .F. ) ;
#248488=DIRECTION ( 'NONE',  ( -1.000000000000000000, 0.000000000000000000, 0.000000000000000000 ) ) ;
#248524=CARTESIAN_POINT ( 'NONE',  ( -14.00000000000000178, 66.15000000001258229, -186.7731074845244166 ) ) ;
#248594=CARTESIAN_POINT ( 'NONE',  ( -16.77683809663752257, 66.05416425680839154, -182.6870565036286393 ) ) ;
#248695=VECTOR ( 'NONE', #119951, 1000.000000000000000 ) ;
#248928=CARTESIAN_POINT ( 'NONE',  ( 20.73486653747090003, 68.75000000001251976, -182.6731074845244223 ) ) ;
#248961=ORIENTED_EDGE ( 'NONE', *, *, #47550, .F. ) ;
#249101=ORIENTED_EDGE ( 'NONE', *, *, #244517, .F. ) ;
#249159=CARTESIAN_POINT ( 'NONE',  ( -16.87998658237756189, 66.05000000001261640, -190.6594679167848767 ) ) ;
#249607=CARTESIAN_POINT ( 'NONE',  ( -16.89268316805466341, 66.04827818677041762, -190.8788599630699707 ) ) ;
#249736=ORIENTED_EDGE ( 'NONE', *, *, #238438, .F. ) ;
#250252=CARTESIAN_POINT ( 'NONE',  ( -33.72168855820452649, 64.52683809665003878, -179.2731074845244450 ) ) ;
#250290=VERTEX_POINT ( 'NONE', #213905 ) ;
#250320=ORIENTED_EDGE ( 'NONE', *, *, #187862, .F. ) ;
#250706=VECTOR ( 'NONE', #61160, 1000.000000000000000 ) ;
#250989=SHAPE_REPRESENTATION_RELATIONSHIP ( 'NONE' , 'NONE' ,  #170171, #237827 ) ;
#251139=CARTESIAN_POINT ( 'NONE',  ( -16.81744102076748959, 66.05000000001255955, -182.6731074845244223 ) ) ;
#251150=DIRECTION ( 'NONE',  ( 0.000000000000000000, -6.982962677686266711E-15, 1.000000000000000000 ) ) ;
#251236=DIRECTION ( 'NONE',  ( 0.000000000000000000, -6.982962677686266711E-15, 1.000000000000000000 ) ) ;
#251414=ADVANCED_FACE ( 'NONE', ( #238651 ), #56139, .F. ) ;
#251623=ORIENTED_EDGE ( 'NONE', *, *, #62454, .T. ) ;
#252083=CARTESIAN_POINT ( 'NONE',  ( 22.88900146558018989, 67.29609520889978569, -190.8731074845244109 ) ) ;
#252223=EDGE_CURVE ( 'NONE', #135464, #13472, #81363, .T. ) ;
#252268=PLANE ( 'NONE',  #26507 ) ;
#252512=VERTEX_POINT ( 'NONE', #128361 ) ;
#252537=VERTEX_POINT ( 'NONE', #221845 ) ;
#252548=ORIENTED_EDGE ( 'NONE', *, *, #149566, .F. ) ;
#252591=CARTESIAN_POINT ( 'NONE',  ( -16.83199030136658081, 66.06935196689912004, -190.7507064618669688 ) ) ;
#252939=FACE_OUTER_BOUND ( 'NONE', #203457, .T. ) ;
#252941=LINE ( 'NONE', #95165, #41141 ) ;
#253103=ORIENTED_EDGE ( 'NONE', *, *, #160897, .T. ) ;
#253507=CARTESIAN_POINT ( 'NONE',  ( 21.72449340488910252, 65.71604372252147641, -190.8731074845244393 ) ) ;
#253873=EDGE_LOOP ( 'NONE', ( #92324, #105572, #90907, #15465 ) ) ;
#254181=EDGE_CURVE ( 'NONE', #103692, #237439, #166968, .T. ) ;
#254191=DIRECTION ( 'NONE',  ( 0.000000000000000000, -6.789366196018718420E-15, 1.000000000000000000 ) ) ;
#254327=PLANE ( 'NONE',  #254981 ) ;
#254377=ORIENTED_EDGE ( 'NONE', *, *, #174875, .F. ) ;
#254693=EDGE_LOOP ( 'NONE', ( #38684, #195656, #29333, #54961 ) ) ;
#254720=ORIENTED_EDGE ( 'NONE', *, *, #237643, .F. ) ;
#254917=CARTESIAN_POINT ( 'NONE',  ( -16.87683809663752399, 66.15000000001255387, -183.4254715027207396 ) ) ;
#254926=DIRECTION ( 'NONE',  ( -1.000000000000000000, 0.000000000000000000, -0.000000000000000000 ) ) ;
#254981=AXIS2_PLACEMENT_3D ( 'NONE', #236066, #233523, #114839 ) ;
#255055=CIRCLE ( 'NONE', #71978, 0.9000000000000014655 ) ;
#255389=VECTOR ( 'NONE', #224990, 1000.000000000000000 ) ;
#255427=ADVANCED_FACE ( 'NONE', ( #179828, #37755, #233392 ), #54721, .T. ) ;
#255557=CARTESIAN_POINT ( 'NONE',  ( -16.93388492042258164, 66.01145817749670641, -190.9236526077106078 ) ) ;
#255888=CARTESIAN_POINT ( 'NONE',  ( 14.22821877134047064, 66.54397173950468414, -188.5119094494587557 ) ) ;
#255913=EDGE_CURVE ( 'NONE', #45497, #219313, #223740, .T. ) ;
#256000=ORIENTED_EDGE ( 'NONE', *, *, #226458, .T. ) ;
#256330=ORIENTED_EDGE ( 'NONE', *, *, #36968, .F. ) ;
#256384=ADVANCED_FACE ( 'NONE', ( #194159 ), #237117, .F. ) ;
#256457=CARTESIAN_POINT ( 'NONE',  ( -16.87331047859651179, 66.05000000001261640, -190.8731074845244393 ) ) ;
#256477=CARTESIAN_POINT ( 'NONE',  ( -18.35235881385853318, 64.52658099229972777, -194.2731074845244450 ) ) ;
#256760=VERTEX_POINT ( 'NONE', #195449 ) ;
#256767=EDGE_CURVE ( 'NONE', #205939, #242970, #247223, .T. ) ;
#256768=EDGE_CURVE ( 'NONE', #2493, #201172, #55652, .T. ) ;
#256836=CARTESIAN_POINT ( 'NONE',  ( -16.92209698673626050, 66.05000000001263061, -190.8124719174703614 ) ) ;
#256856=EDGE_CURVE ( 'NONE', #45497, #157258, #243530, .T. ) ;
#256990=EDGE_CURVE ( 'NONE', #166894, #6267, #186128, .T. ) ;
#257341=CARTESIAN_POINT ( 'NONE',  ( 18.39999999999999503, 64.25000000001256240, -182.6731074845244507 ) ) ;
#257369=CARTESIAN_POINT ( 'NONE',  ( -16.89268316805465986, 66.04827818677036078, -182.6673550059788909 ) ) ;
#257619=CARTESIAN_POINT ( 'NONE',  ( -18.35668295345803713, 64.52683809665005299, -179.2731074845244450 ) ) ;
#257704=VECTOR ( 'NONE', #174663, 999.9999999999998863 ) ;
#258007=( BOUNDED_CURVE ( )  B_SPLINE_CURVE ( 3, ( #191562, #69038, #12926, #76703 ),
 .UNSPECIFIED., .F., .F. ) 
 B_SPLINE_CURVE_WITH_KNOTS ( ( 4, 4 ),
 ( 1.570796326794908992, 2.617993877991549034 ),
 .UNSPECIFIED. ) 
 CURVE ( )  GEOMETRIC_REPRESENTATION_ITEM ( )  RATIONAL_B_SPLINE_CURVE ( ( 1.000000000000000000, 0.9106836025229521070, 0.9106836025229521070, 1.000000000000000000 ) ) 
 REPRESENTATION_ITEM ( '' )  );
#258026=EDGE_CURVE ( 'NONE', #76104, #130997, #66225, .T. ) ;
#258033=DIRECTION ( 'NONE',  ( -0.5932847527679310229, -0.8049926720990042694, -4.984624513800578906E-15 ) ) ;
ENDSEC;
END-ISO-10303-21;
